ISO-10303-21;
HEADER;
FILE_DESCRIPTION (('STEP AP203'),
    '1' );
FILE_NAME ('Aloris-BXA-Center-Shaft.step',
    '2026-10-07T20:09:13',
    ( '' ),
    ( '' ),
    'SwSTEP 2.0',
    'SolidWorks 2024',
    '' );
FILE_SCHEMA (( 'AUTOMOTIVE_DESIGN' ));
ENDSEC;

DATA;
#2=CARTESIAN_POINT ( 'NONE',  ( 0.2472135954999579721, 0.2589285712334865597, -0.3402603233408160732 ) ) ;
#10=EDGE_LOOP ( 'NONE', ( #22952, #23835 ) ) ;
#14=CARTESIAN_POINT ( 'NONE',  ( -0.3236067977499789694, 0.1428571428571428215, -0.2351141009169893104 ) ) ;
#23=CARTESIAN_POINT ( 'NONE',  ( -0.4000000000000000222, 0.06964285694777234970, -4.898587196589413075E-17 ) ) ;
#24=CARTESIAN_POINT ( 'NONE',  ( 0.1554777997599670336, -3.800488706749824749E-17, -0.3394405886668848682 ) ) ;
#45=VERTEX_POINT ( 'NONE', #6974 ) ;
#46=DIRECTION ( 'NONE',  ( 0.000000000000000000, 0.000000000000000000, -1.000000000000000000 ) ) ;
#48=CARTESIAN_POINT ( 'NONE',  ( -0.1116596296178200276, 0.04374999990245760639, 0.3436530038418508792 ) ) ;
#51=CARTESIAN_POINT ( 'NONE',  ( 0.3613381517857143232, 0.08660714275960043618, -0.1174058825155740587 ) ) ;
#61=EDGE_CURVE ( 'NONE', #19679, #20558, #12738, .T. ) ;
#66=EDGE_LOOP ( 'NONE', ( #14998, #20561, #21029, #16643 ) ) ;
#67=CARTESIAN_POINT ( 'NONE',  ( 0.2923287055106771337, 0.2008928570453147044, 0.2123892367102621359 ) ) ;
#86=LINE ( 'NONE', #23728, #15966 ) ;
#106=CARTESIAN_POINT ( 'NONE',  ( 0.3613381517857143232, 0.3723214284738861068, -0.1174058825155740587 ) ) ;
#117=CARTESIAN_POINT ( 'NONE',  ( -0.2923287055106771337, 0.2687499999024575703, 0.2123892367102619971 ) ) ;
#121=CARTESIAN_POINT ( 'NONE',  ( 0.3587893197688488689, 1.447158556123030749E-17, -0.04444430867843930655 ) ) ;
#126=ADVANCED_FACE ( 'NONE', ( #2334 ), #2953, .F. ) ;
#136=ORIENTED_EDGE ( 'NONE', *, *, #22688, .T. ) ;
#140=CARTESIAN_POINT ( 'NONE',  ( 0.4000000000000000222, 0.1142857142857142405, 0.000000000000000000 ) ) ;
#147=CARTESIAN_POINT ( 'NONE',  ( -0.1236067977499789583, 0.1267857140906294977, -0.3804226065180614791 ) ) ;
#171=CARTESIAN_POINT ( 'NONE',  ( 0.2923287055106771337, -0.01339285724039953988, 0.2123892367102621359 ) ) ;
#174=CARTESIAN_POINT ( 'NONE',  ( 2.326421213736078119E-17, 0.02946428561674332633, -0.3799334167787516980 ) ) ;
#179=EDGE_CURVE ( 'NONE', #769, #10349, #4149, .T. ) ;
#187=CARTESIAN_POINT ( 'NONE',  ( -0.4749999999999999778, 3.575000000000000622, -0.09499999999999995948 ) ) ;
#189=CARTESIAN_POINT ( 'NONE',  ( -6.979263641208234666E-17, 0.1901785713310290005, 0.3799334167787516980 ) ) ;
#201=CARTESIAN_POINT ( 'NONE',  ( -0.1116596296178199582, 0.3723214284738861068, -0.3436530038418508792 ) ) ;
#216=CARTESIAN_POINT ( 'NONE',  ( -0.4000000000000000222, 0.2964285714285713191, 0.1299678784931624920 ) ) ;
#233=CARTESIAN_POINT ( 'NONE',  ( -0.3613381517857143232, 0.1901785713310290005, -4.425116109941954795E-17 ) ) ;
#247=CARTESIAN_POINT ( 'NONE',  ( -9.626299801968715084E-16, 0.4089285712334866374, -0.4000000000000000222 ) ) ;
#262=CARTESIAN_POINT ( 'NONE',  ( -0.3949525857693607089, 5.436648244187127775E-19, 0.06334394204733222178 ) ) ;
#263=CARTESIAN_POINT ( 'NONE',  ( -7.726019084026502927E-17, 0.1678571428571428159, 0.4205848896953069405 ) ) ;
#271=CARTESIAN_POINT ( 'NONE',  ( -0.3236067977499790249, 0.1482142855192009057, 0.2351141009169892271 ) ) ;
#282=CARTESIAN_POINT ( 'NONE',  ( 0.06335377612981443751, 0.4464733670030167634, 0.4000000000000000222 ) ) ;
#292=CARTESIAN_POINT ( 'NONE',  ( -0.3613381517857144343, -0.03839285724039952913, 0.1174058825155740171 ) ) ;
#297=CARTESIAN_POINT ( 'NONE',  ( 0.2923287055106771337, 0.1616071427596004473, -0.2123892367102620249 ) ) ;
#306=ORIENTED_EDGE ( 'NONE', *, *, #17817, .T. ) ;
#309=AXIS2_PLACEMENT_3D ( 'NONE', #6087, #20725, #7680 ) ;
#312=CARTESIAN_POINT ( 'NONE',  ( -0.2233192592356399442, 0.09017857133102903655, -0.3073725909049499494 ) ) ;
#329=CARTESIAN_POINT ( 'NONE',  ( 0.4000000000000000222, 0.4312499999024575481, 0.000000000000000000 ) ) ;
#331=CARTESIAN_POINT ( 'NONE',  ( -0.3341642768485558745, -2.437189573335733509E-18, 0.2058836888633447382 ) ) ;
#336=CARTESIAN_POINT ( 'NONE',  ( -0.2472135954999579999, 0.2321428571428570953, 0.3402603233408160732 ) ) ;
#349=CARTESIAN_POINT ( 'NONE',  ( 0.2923287055106771337, 0.07232142847388615958, -0.2123892367102620249 ) ) ;
#356=CARTESIAN_POINT ( 'NONE',  ( -4.638126268221291196E-16, 0.1232142855192009251, -0.4000000000000000222 ) ) ;
#359=VECTOR ( 'NONE', #7584, 39.37007874015748143 ) ;
#365=CARTESIAN_POINT ( 'NONE',  ( 0.3236067977499789694, 0.3124999998049152183, 0.2351141009169893659 ) ) ;
#382=CARTESIAN_POINT ( 'NONE',  ( 0.1236067977499789028, 0.1714285714285714024, 0.3804226065180614791 ) ) ;
#391=CARTESIAN_POINT ( 'NONE',  ( -0.2472135954999579444, 0.4160714283763436994, -0.3402603233408159622 ) ) ;
#411=VECTOR ( 'NONE', #12252, 39.37007874015748143 ) ;
#416=CARTESIAN_POINT ( 'NONE',  ( 0.2233192592356399164, 0.1258928570453146933, 0.3073725909049500604 ) ) ;
#419=CARTESIAN_POINT ( 'NONE',  ( 0.3613381517857143232, 0.2973214284738861513, 0.000000000000000000 ) ) ;
#431=VERTEX_POINT ( 'NONE', #4509 ) ;
#432=CARTESIAN_POINT ( 'NONE',  ( -0.1116596296178200276, 0.04374999990245760639, 0.3436530038418508792 ) ) ;
#437=( BOUNDED_CURVE ( )  B_SPLINE_CURVE ( 2, ( #13480, #7963, #15531, #17360, #652, #13716, #4550, #12013, #19425 ),
 .UNSPECIFIED., .F., .F. ) 
 B_SPLINE_CURVE_WITH_KNOTS ( ( 3, 2, 2, 2, 3 ),
 ( 0.2000000000000000111, 0.2142857142857142738, 0.2285714285714285643, 0.2428571428571428548, 0.2500000000000000000 ),
 .UNSPECIFIED. ) 
 CURVE ( )  GEOMETRIC_REPRESENTATION_ITEM ( )  RATIONAL_B_SPLINE_CURVE ( ( 1.000000000000000000, 0.9510565162951535312, 1.000000000000000000, 0.9510565162951535312, 1.000000000000000000, 0.9510565162951535312, 1.000000000000000000, 0.9755282581475767101, 0.9755282581475768211 ) ) 
 REPRESENTATION_ITEM ( '' )  );
#439=DIRECTION ( 'NONE',  ( 0.000000000000000000, 0.000000000000000000, 1.000000000000000000 ) ) ;
#453=CARTESIAN_POINT ( 'NONE',  ( -0.1385944955600183770, -6.721771644360946285E-18, 0.3536177551490795046 ) ) ;
#468=CARTESIAN_POINT ( 'NONE',  ( -6.979263641208234666E-17, -0.02410714295468524906, 0.3799334167787516425 ) ) ;
#483=CARTESIAN_POINT ( 'NONE',  ( 0.06335377612981493711, 0.3750447955744454220, 0.3999999999999999667 ) ) ;
#485=CARTESIAN_POINT ( 'NONE',  ( 0.06335377612981453466, 0.3356694897496707020, -0.3999999999999999667 ) ) ;
#499=CARTESIAN_POINT ( 'NONE',  ( 4.375590819076689459E-17, 0.01607142837634377430, 0.4000000000000000222 ) ) ;
#500=CARTESIAN_POINT ( 'NONE',  ( -0.1236067977499790416, 0.3071428571428570509, 0.3804226065180614236 ) ) ;
#502=CIRCLE ( 'NONE', #21150, 0.3125000000000000000 ) ;
#508=CARTESIAN_POINT ( 'NONE',  ( -0.2472135954999579444, 0.2017857140906294255, -0.3402603233408159622 ) ) ;
#516=VECTOR ( 'NONE', #6210, 39.37007874015748143 ) ;
#529=CARTESIAN_POINT ( 'NONE',  ( 0.000000000000000000, 3.700000000000000622, 0.000000000000000000 ) ) ;
#531=CARTESIAN_POINT ( 'NONE',  ( 0.1116596296178199860, 0.1508928570453147155, -0.3436530038418508792 ) ) ;
#534=CARTESIAN_POINT ( 'NONE',  ( 0.2233192592356399164, 0.2866071427596003640, 0.3073725909049500604 ) ) ;
#547=CARTESIAN_POINT ( 'NONE',  ( 0.2233192592356399164, 0.1973214284738861179, 0.3073725909049500604 ) ) ;
#565=CARTESIAN_POINT ( 'NONE',  ( -0.2472135954999579444, 0.4160714283763437549, -0.3402603233408160732 ) ) ;
#568=LINE ( 'NONE', #329, #15357 ) ;
#578=CYLINDRICAL_SURFACE ( 'NONE', #9347, 0.4000000000000000222 ) ;
#589=CARTESIAN_POINT ( 'NONE',  ( -0.2923287055106771337, -0.04910714295468524004, -0.2123892367102620804 ) ) ;
#595=ORIENTED_EDGE ( 'NONE', *, *, #6816, .T. ) ;
#599=CARTESIAN_POINT ( 'NONE',  ( 0.2752577204847949655, 1.857579423845309578E-17, -0.2411543459231450526 ) ) ;
#603=FACE_OUTER_BOUND ( 'NONE', #11639, .T. ) ;
#610=CIRCLE ( 'NONE', #7625, 0.3125000000000000000 ) ;
#611=CARTESIAN_POINT ( 'NONE',  ( 0.2233192592356400275, 0.3616071427596003751, -0.3073725909049499494 ) ) ;
#626=CARTESIAN_POINT ( 'NONE',  ( -0.3236067977499789694, 0.1428571428571428215, -0.2351141009169893104 ) ) ;
#634=CARTESIAN_POINT ( 'NONE',  ( -0.3236067977499789694, 0.2767857140906295199, -0.2351141009169893104 ) ) ;
#647=CARTESIAN_POINT ( 'NONE',  ( 0.06335377612981493711, 0.3125447957695302037, 0.3999999999999999667 ) ) ;
#652=CARTESIAN_POINT ( 'NONE',  ( -0.3236067977499790249, 0.01428571428571426098, 0.2351141009169892271 ) ) ;
#655=CARTESIAN_POINT ( 'NONE',  ( 0.1116596296178199860, 0.2937499999024575925, -0.3436530038418508792 ) ) ;
#672=CARTESIAN_POINT ( 'NONE',  ( -0.2923287055106771337, 0.2366071427596004584, -0.2123892367102620804 ) ) ;
#694=CARTESIAN_POINT ( 'NONE',  ( -0.3775338486402941007, 2.665439728940100056E-18, 0.1233678446911569832 ) ) ;
#710=CARTESIAN_POINT ( 'NONE',  ( 0.3613381517857143232, 0.4401785713310289450, 0.000000000000000000 ) ) ;
#717=DIRECTION ( 'NONE',  ( -0.000000000000000000, 0.000000000000000000, 1.000000000000000000 ) ) ;
#719=CARTESIAN_POINT ( 'NONE',  ( -0.3236067977499789694, -1.707404996040164512E-17, -0.2351141009169893104 ) ) ;
#731=CARTESIAN_POINT ( 'NONE',  ( -6.979263641208234666E-17, 0.3330357141881718497, 0.3799334167787516980 ) ) ;
#741=AXIS2_PLACEMENT_3D ( 'NONE', #23126, #21197, #4488 ) ;
#745=CARTESIAN_POINT ( 'NONE',  ( -0.1236067977499789583, 0.3499999999999998668, -0.3804226065180614791 ) ) ;
#752=CARTESIAN_POINT ( 'NONE',  ( -0.4000000000000000222, 0.2124999998049151573, -4.898587196589413075E-17 ) ) ;
#755=ORIENTED_EDGE ( 'NONE', *, *, #13785, .F. ) ;
#764=ORIENTED_EDGE ( 'NONE', *, *, #8568, .T. ) ;
#769=VERTEX_POINT ( 'NONE', #23119 ) ;
#771=DIRECTION ( 'NONE',  ( -0.000000000000000000, -1.000000000000000000, -0.000000000000000000 ) ) ;
#773=CARTESIAN_POINT ( 'NONE',  ( 0.2233192592356399997, 0.3616071427596004861, -0.3073725909049500049 ) ) ;
#777=CARTESIAN_POINT ( 'NONE',  ( 0.2233192592356399164, 0.4294642856167432687, 0.3073725909049500604 ) ) ;
#779=CARTESIAN_POINT ( 'NONE',  ( -0.2472135954999579444, 0.1303571426620580564, -0.3402603233408160732 ) ) ;
#806=ORIENTED_EDGE ( 'NONE', *, *, #16313, .F. ) ;
#809=DIRECTION ( 'NONE',  ( -0.000000000000000000, -1.000000000000000000, -0.000000000000000000 ) ) ;
#829=CARTESIAN_POINT ( 'NONE',  ( -0.3613381517857143232, -0.04196428581182810175, -4.425116109941954795E-17 ) ) ;
#832=CARTESIAN_POINT ( 'NONE',  ( 4.113055369932088708E-16, 0.09642857142857140518, 0.4000000000000000222 ) ) ;
#839=CARTESIAN_POINT ( 'NONE',  ( 0.2078702321837838651, 1.046010598739760082E-17, -0.3061389487775396656 ) ) ;
#846=CARTESIAN_POINT ( 'NONE',  ( 0.2630554106833125072, -9.196729208309143084E-18, 0.2488419919605451280 ) ) ;
#851=CARTESIAN_POINT ( 'NONE',  ( 0.2977100099089716734, 3.575000000000000622, 0.09499999999999993172 ) ) ;
#859=CARTESIAN_POINT ( 'NONE',  ( 0.1236067977499789028, 0.2428571428571427715, 0.3804226065180614791 ) ) ;
#861=CARTESIAN_POINT ( 'NONE',  ( 0.000000000000000000, 3.659999999999999698, 0.3125000000000000000 ) ) ;
#870=CARTESIAN_POINT ( 'NONE',  ( -0.4000000000000000222, 0.2874999998049151961, 0.1299678784931624920 ) ) ;
#892=LINE ( 'NONE', #4427, #411 ) ;
#893=CARTESIAN_POINT ( 'NONE',  ( -0.2923287055106771337, 0.1794642856167432687, 0.2123892367102619971 ) ) ;
#896=CARTESIAN_POINT ( 'NONE',  ( -0.2233192592356399442, 0.3223214284738860624, -0.3073725909049499494 ) ) ;
#897=CARTESIAN_POINT ( 'NONE',  ( -0.2472135954999579999, 0.1517857140906294644, 0.3402603233408160732 ) ) ;
#909=EDGE_LOOP ( 'NONE', ( #6397, #21370, #16740, #1085, #21888 ) ) ;
#918=FACE_OUTER_BOUND ( 'NONE', #18485, .T. ) ;
#927=LINE ( 'NONE', #2761, #14505 ) ;
#935=EDGE_CURVE ( 'NONE', #4205, #15982, #6797, .T. ) ;
#941=CARTESIAN_POINT ( 'NONE',  ( 0.2233192592356399164, 0.1973214284738861179, 0.3073725909049500604 ) ) ;
#964=CARTESIAN_POINT ( 'NONE',  ( 0.2923287055106771337, 0.0008928570453147542749, -0.2123892367102620249 ) ) ;
#976=CARTESIAN_POINT ( 'NONE',  ( 0.4000000000000000222, 0.3999999999999999112, 0.000000000000000000 ) ) ;
#979=CARTESIAN_POINT ( 'NONE',  ( 0.3613381517857143232, 0.08660714275960043618, -0.1174058825155740587 ) ) ;
#991=CARTESIAN_POINT ( 'NONE',  ( 0.3236067977499789694, 0.4553571426620580120, 0.2351141009169893659 ) ) ;
#996=CARTESIAN_POINT ( 'NONE',  ( 4.113055369932088708E-16, 0.1589285712334866096, 0.4000000000000000222 ) ) ;
#1002=( NAMED_UNIT ( * ) SI_UNIT ( $, .STERADIAN. ) SOLID_ANGLE_UNIT ( ) );
#1016=CARTESIAN_POINT ( 'NONE',  ( -6.979263641208234666E-17, 0.3330357141881717942, 0.3799334167787516425 ) ) ;
#1045=ORIENTED_EDGE ( 'NONE', *, *, #19956, .T. ) ;
#1047=CARTESIAN_POINT ( 'NONE',  ( 0.000000000000000000, 3.659999999999999698, 0.000000000000000000 ) ) ;
#1067=CARTESIAN_POINT ( 'NONE',  ( 0.2923287055106771337, 0.2151785713310289949, -0.2123892367102620249 ) ) ;
#1072=ORIENTED_EDGE ( 'NONE', *, *, #5116, .T. ) ;
#1075=CARTESIAN_POINT ( 'NONE',  ( 0.06335377612981468731, 0.09825908148381588825, 0.3999999999999999667 ) ) ;
#1082=MANIFOLD_SOLID_BREP ( 'Thread1', #19696 ) ;
#1085=ORIENTED_EDGE ( 'NONE', *, *, #14542, .F. ) ;
#1099=CARTESIAN_POINT ( 'NONE',  ( -0.1116596296178199582, 0.1044642856167432993, -0.3436530038418508792 ) ) ;
#1104=CARTESIAN_POINT ( 'NONE',  ( 2.575339694675500462E-17, 0.3464285714285712525, -0.4205848896953069405 ) ) ;
#1114=CARTESIAN_POINT ( 'NONE',  ( 0.2233192592356399997, -0.04910714295468524698, -0.3073725909049500049 ) ) ;
#1133=EDGE_LOOP ( 'NONE', ( #17618, #3765, #23247, #17240, #2720 ) ) ;
#1138=CARTESIAN_POINT ( 'NONE',  ( -0.3613381517857143232, 0.1723214284738861513, -4.425116109941954795E-17 ) ) ;
#1149=CARTESIAN_POINT ( 'NONE',  ( -7.000945310522701902E-17, 0.2303571426620580065, 0.3999999999999999667 ) ) ;
#1165=CARTESIAN_POINT ( 'NONE',  ( -0.3236067977499789694, 0.3571428571428570398, -0.2351141009169893104 ) ) ;
#1187=CARTESIAN_POINT ( 'NONE',  ( -6.979263641208234666E-17, 0.3508928570453145879, 0.3799334167787516425 ) ) ;
#1191=CARTESIAN_POINT ( 'NONE',  ( 0.2923287055106771337, 0.2866071427596004195, -0.2123892367102620249 ) ) ;
#1210=CARTESIAN_POINT ( 'NONE',  ( 4.194415287079685308E-17, 0.02999999999999995379, -0.3425000000000000266 ) ) ;
#1223=CARTESIAN_POINT ( 'NONE',  ( -0.1116596296178200276, 0.06160714275960045561, 0.3436530038418508792 ) ) ;
#1237=CARTESIAN_POINT ( 'NONE',  ( -0.4000000000000000222, 0.4303571426620579898, 0.1299678784931624920 ) ) ;
#1257=CARTESIAN_POINT ( 'NONE',  ( -0.2472135954999579444, -0.07500000000000002498, -0.3402603233408159622 ) ) ;
#1258=CARTESIAN_POINT ( 'NONE',  ( 0.000000000000000000, 3.700000000000000622, 0.000000000000000000 ) ) ;
#1259=EDGE_CURVE ( 'NONE', #1426, #16231, #1475, .T. ) ;
#1260=CARTESIAN_POINT ( 'NONE',  ( 0.000000000000000000, 0.000000000000000000, 0.000000000000000000 ) ) ;
#1265=CARTESIAN_POINT ( 'NONE',  ( -0.3949525857693607089, 5.436648244187127775E-19, 0.06334394204733222178 ) ) ;
#1270=DIRECTION ( 'NONE',  ( -0.000000000000000000, 1.000000000000000000, -0.000000000000000000 ) ) ;
#1289=ORIENTED_EDGE ( 'NONE', *, *, #20498, .F. ) ;
#1309=EDGE_CURVE ( 'NONE', #16532, #21451, #8806, .T. ) ;
#1312=CARTESIAN_POINT ( 'NONE',  ( 0.2233192592356399164, 0.2687499999024575703, 0.3073725909049500604 ) ) ;
#1338=CYLINDRICAL_SURFACE ( 'NONE', #15578, 0.09499999999999995948 ) ;
#1340=CARTESIAN_POINT ( 'NONE',  ( 0.3613381517857143232, 0.01160714275960045803, 0.000000000000000000 ) ) ;
#1353=CARTESIAN_POINT ( 'NONE',  ( -0.2923287055106771337, 0.04017857133102904071, -0.2123892367102620804 ) ) ;
#1375=ORIENTED_EDGE ( 'NONE', *, *, #20910, .T. ) ;
#1379=CARTESIAN_POINT ( 'NONE',  ( -0.4000000000000000222, 0.07857142857142855596, -4.898587196589413075E-17 ) ) ;
#1387=CARTESIAN_POINT ( 'NONE',  ( 0.000000000000000000, 2.735000000000000320, 0.000000000000000000 ) ) ;
#1391=CARTESIAN_POINT ( 'NONE',  ( -4.638126268221291196E-16, 0.1946428569477723358, -0.4000000000000000222 ) ) ;
#1401=CARTESIAN_POINT ( 'NONE',  ( -0.4749999999999999778, 3.575000000000000622, 0.09499999999999995948 ) ) ;
#1409=CARTESIAN_POINT ( 'NONE',  ( -0.3236067977499790249, 0.3714285714285713302, 0.2351141009169892271 ) ) ;
#1426=VERTEX_POINT ( 'NONE', #6862 ) ;
#1432=CARTESIAN_POINT ( 'NONE',  ( -0.2923287055106771337, 0.3258928570453146767, -0.2123892367102620804 ) ) ;
#1435=CARTESIAN_POINT ( 'NONE',  ( -0.1116596296178200276, 0.1151785713310290032, 0.3436530038418508792 ) ) ;
#1439=CARTESIAN_POINT ( 'NONE',  ( -0.4749999999999999778, 3.700000000000000622, 0.09499999999999995948 ) ) ;
#1444=VECTOR ( 'NONE', #19758, 39.37007874015748854 ) ;
#1461=CYLINDRICAL_SURFACE ( 'NONE', #22916, 0.4000000000000000222 ) ;
#1462=CARTESIAN_POINT ( 'NONE',  ( -0.3613381517857144343, -0.02053571438325667298, 0.1174058825155740171 ) ) ;
#1465=CARTESIAN_POINT ( 'NONE',  ( 0.4000000000000000222, 0.03392857123348663045, 0.000000000000000000 ) ) ;
#1474=CARTESIAN_POINT ( 'NONE',  ( -0.2233192592356399442, 0.1080357141881718996, -0.3073725909049500049 ) ) ;
#1475=LINE ( 'NONE', #24024, #19713 ) ;
#1482=EDGE_CURVE ( 'NONE', #18107, #16753, #18437, .T. ) ;
#1486=CARTESIAN_POINT ( 'NONE',  ( 0.3236067977499789694, 0.1785714285714284921, 0.2351141009169893659 ) ) ;
#1498=CARTESIAN_POINT ( 'NONE',  ( 2.575339694675500462E-17, -0.01071428571428573000, -0.4205848896953069405 ) ) ;
#1534=DIRECTION ( 'NONE',  ( 0.000000000000000000, 1.000000000000000000, 0.000000000000000000 ) ) ;
#1544=DIRECTION ( 'NONE',  ( 0.000000000000000000, -0.000000000000000000, 1.000000000000000000 ) ) ;
#1551=CARTESIAN_POINT ( 'NONE',  ( 0.2472135954999579166, 0.03214285714285712581, 0.3402603233408160732 ) ) ;
#1556=LINE ( 'NONE', #1439, #18274 ) ;
#1575=AXIS2_PLACEMENT_3D ( 'NONE', #7907, #4256, #23613 ) ;
#1582=LINE ( 'NONE', #14762, #16305 ) ;
#1583=CARTESIAN_POINT ( 'NONE',  ( 0.2923287055106771337, 0.3044642856167432687, -0.2123892367102620249 ) ) ;
#1597=CARTESIAN_POINT ( 'NONE',  ( -0.1116596296178199582, 0.2473214284738861346, -0.3436530038418508792 ) ) ;
#1608=CARTESIAN_POINT ( 'NONE',  ( -7.000945310522701902E-17, 0.1678571428571427882, 0.3999999999999999667 ) ) ;
#1612=DIRECTION ( 'NONE',  ( 0.000000000000000000, 1.000000000000000000, 0.000000000000000000 ) ) ;
#1615=EDGE_CURVE ( 'NONE', #16849, #21333, #8833, .T. ) ;
#1618=CARTESIAN_POINT ( 'NONE',  ( 0.1236067977499789861, -0.08571428571428572896, -0.3804226065180614236 ) ) ;
#1624=CARTESIAN_POINT ( 'NONE',  ( -0.3236067977499790249, 0.07678571409062949493, 0.2351141009169892271 ) ) ;
#1630=CARTESIAN_POINT ( 'NONE',  ( -0.3255746755405797832, 3.686631053106446565, -0.09499999999999995948 ) ) ;
#1642=FACE_OUTER_BOUND ( 'NONE', #4880, .T. ) ;
#1647=CARTESIAN_POINT ( 'NONE',  ( 0.1116596296178199860, 0.2401785713310289616, -0.3436530038418508792 ) ) ;
#1691=DIRECTION ( 'NONE',  ( 0.000000000000000000, 1.000000000000000000, 0.000000000000000000 ) ) ;
#1698=CARTESIAN_POINT ( 'NONE',  ( -0.1116596296178199582, 0.2473214284738861346, -0.3436530038418508792 ) ) ;
#1711=CARTESIAN_POINT ( 'NONE',  ( -0.2923287055106771337, 0.1973214284738861179, 0.2123892367102619971 ) ) ;
#1720=CIRCLE ( 'NONE', #7177, 0.3425000000000000266 ) ;
#1723=APPLICATION_CONTEXT ( 'configuration controlled 3d designs of mechanical parts and assemblies' ) ;
#1734=CARTESIAN_POINT ( 'NONE',  ( -0.2472135954999579444, -0.003571428571428599073, -0.3402603233408159622 ) ) ;
#1740=CARTESIAN_POINT ( 'NONE',  ( 0.3236067977499790249, -0.03035714305222763157, -0.2351141009169892826 ) ) ;
#1747=CARTESIAN_POINT ( 'NONE',  ( -0.3394572874457115752, 3.700000000000000622, -0.09499999999999993172 ) ) ;
#1766=CARTESIAN_POINT ( 'NONE',  ( -0.2233192592356400275, 0.05803571418817188299, 0.3073725909049499494 ) ) ;
#1774=CARTESIAN_POINT ( 'NONE',  ( 0.3806690758928571450, 0.4111607142369430590, 0.000000000000000000 ) ) ;
#1778=DIRECTION ( 'NONE',  ( 0.000000000000000000, 0.000000000000000000, -1.000000000000000000 ) ) ;
#1788=CARTESIAN_POINT ( 'NONE',  ( 0.3999999999999999667, 0.03928571428571425023, 0.1299678784931626307 ) ) ;
#1801=CARTESIAN_POINT ( 'NONE',  ( 4.898587196589413075E-17, 3.700000000000000622, 0.4000000000000000222 ) ) ;
#1813=CARTESIAN_POINT ( 'NONE',  ( 0.3613381517857143232, 0.2223214284738861402, 0.1174058825155742114 ) ) ;
#1826=CARTESIAN_POINT ( 'NONE',  ( 0.1116596296178199027, 0.2116071427596004639, 0.3436530038418508792 ) ) ;
#1837=CARTESIAN_POINT ( 'NONE',  ( 0.4000000000000000222, 0.2482142855192008835, 0.000000000000000000 ) ) ;
#1838=CARTESIAN_POINT ( 'NONE',  ( 0.2472135954999579166, 0.1749999999999999889, 0.3402603233408160732 ) ) ;
#1848=CARTESIAN_POINT ( 'NONE',  ( -0.06335377612981410445, 0.3713837754639563449, 0.4000000000000001887 ) ) ;
#1849=CARTESIAN_POINT ( 'NONE',  ( 0.4000000000000000222, 0.1857142857142856651, 0.000000000000000000 ) ) ;
#1857=CARTESIAN_POINT ( 'NONE',  ( 0.2472135954999579721, -0.02678571448079906589, -0.3402603233408159622 ) ) ;
#1858=CARTESIAN_POINT ( 'NONE',  ( 4.113055369932088708E-16, 0.1589285712334866096, 0.4000000000000000222 ) ) ;
#1869=CARTESIAN_POINT ( 'NONE',  ( -0.06335377612981410445, 0.2999552040353848925, 0.4000000000000001887 ) ) ;
#1882=CARTESIAN_POINT ( 'NONE',  ( -4.638126268221291196E-16, 0.1232142855192009251, -0.4000000000000000222 ) ) ;
#1887=CARTESIAN_POINT ( 'NONE',  ( 0.2233192592356399164, 0.1437499999024575703, 0.3073725909049500604 ) ) ;
#1891=EDGE_CURVE ( 'NONE', #6978, #18107, #6506, .T. ) ;
#1902=CARTESIAN_POINT ( 'NONE',  ( -6.979263641208234666E-17, 0.04732142847388615819, 0.3799334167787516980 ) ) ;
#1907=CIRCLE ( 'NONE', #16711, 0.3125000000000000000 ) ;
#1916=ADVANCED_FACE ( 'NONE', ( #20983 ), #15148, .F. ) ;
#1920=DIRECTION ( 'NONE',  ( 0.000000000000000000, -1.000000000000000000, 0.000000000000000000 ) ) ;
#1936=CARTESIAN_POINT ( 'NONE',  ( 0.2233192592356399164, 0.2866071427596003640, 0.3073725909049500604 ) ) ;
#1937=AXIS2_PLACEMENT_3D ( 'NONE', #23115, #19230, #4353 ) ;
#1948=CARTESIAN_POINT ( 'NONE',  ( 0.2233192592356399997, 0.3080357141881718275, -0.3073725909049500049 ) ) ;
#1953=CARTESIAN_POINT ( 'NONE',  ( 0.3473794045410782405, -4.100712535614411444E-18, -0.1022067409664305093 ) ) ;
#1966=CARTESIAN_POINT ( 'NONE',  ( 0.3999999999999999667, 0.1892857142857141961, -0.1299678784931625197 ) ) ;
#1973=EDGE_LOOP ( 'NONE', ( #14961, #7082 ) ) ;
#1978=CARTESIAN_POINT ( 'NONE',  ( -0.4000000000000000222, 0.2964285714285713191, 0.1299678784931624920 ) ) ;
#1987=CARTESIAN_POINT ( 'NONE',  ( -0.4000000000000000222, 0.1410714283763437882, -4.898587196589413075E-17 ) ) ;
#2009=CARTESIAN_POINT ( 'NONE',  ( -6.979263641208234666E-17, 0.1187499999024575897, 0.3799334167787516425 ) ) ;
#2013=CARTESIAN_POINT ( 'NONE',  ( 0.1116596296178199027, 0.06874999990245758696, 0.3436530038418508792 ) ) ;
#2025=CARTESIAN_POINT ( 'NONE',  ( -0.2233192592356399442, 0.2330357141881718719, -0.3073725909049499494 ) ) ;
#2030=EDGE_CURVE ( 'NONE', #21724, #2478, #12342, .T. ) ;
#2040=CARTESIAN_POINT ( 'NONE',  ( -0.1236067977499789583, 0.4124999998049150851, -0.3804226065180614791 ) ) ;
#2060=CARTESIAN_POINT ( 'NONE',  ( -0.3613381517857144343, 0.1937499999024575870, 0.1174058825155740171 ) ) ;
#2073=FACE_OUTER_BOUND ( 'NONE', #4142, .T. ) ;
#2093=CARTESIAN_POINT ( 'NONE',  ( 0.3236067977499790249, 0.1214285714285713996, -0.2351141009169892826 ) ) ;
#2096=ADVANCED_FACE ( 'NONE', ( #3167 ), #18047, .T. ) ;
#2101=CARTESIAN_POINT ( 'NONE',  ( 0.2472135954999579166, 0.02321428551920093342, 0.3402603233408160732 ) ) ;
#2105=DIRECTION ( 'NONE',  ( 0.000000000000000000, 0.000000000000000000, -1.000000000000000000 ) ) ;
#2110=CIRCLE ( 'NONE', #18838, 0.4000000000000000222 ) ;
#2111=CARTESIAN_POINT ( 'NONE',  ( -9.626299801968715084E-16, 0.2660714283763437327, -0.4000000000000000222 ) ) ;
#2118=VERTEX_POINT ( 'NONE', #13799 ) ;
#2126=CARTESIAN_POINT ( 'NONE',  ( -0.3613381517857143232, 0.09732142847388615403, -0.1174058825155741004 ) ) ;
#2130=CARTESIAN_POINT ( 'NONE',  ( 0.2233192592356399164, 0.2151785713310289949, 0.3073725909049500604 ) ) ;
#2132=CARTESIAN_POINT ( 'NONE',  ( 0.000000000000000000, 3.659999999999999698, 0.000000000000000000 ) ) ;
#2148=CARTESIAN_POINT ( 'NONE',  ( -0.2233192592356400275, 0.1116071427596004445, 0.3073725909049499494 ) ) ;
#2183=ORIENTED_EDGE ( 'NONE', *, *, #14379, .T. ) ;
#2192=CARTESIAN_POINT ( 'NONE',  ( -0.2233192592356399442, -0.05267857152611380572, -0.3073725909049500049 ) ) ;
#2208=ORIENTED_EDGE ( 'NONE', *, *, #10822, .T. ) ;
#2209=CARTESIAN_POINT ( 'NONE',  ( 0.06335377612981493711, 0.3036162241458739697, 0.3999999999999999667 ) ) ;
#2211=CARTESIAN_POINT ( 'NONE',  ( 0.3613381517857143232, 0.4187499999024575370, 0.1174058825155741975 ) ) ;
#2226=CARTESIAN_POINT ( 'NONE',  ( 0.2472135954999579721, 0.2678571428571427382, -0.3402603233408159622 ) ) ;
#2233=CARTESIAN_POINT ( 'NONE',  ( 0.3999999999999999667, 0.3232142855192008946, -0.1299678784931625475 ) ) ;
#2253=DIRECTION ( 'NONE',  ( 0.000000000000000000, 1.000000000000000000, 0.000000000000000000 ) ) ;
#2254=CARTESIAN_POINT ( 'NONE',  ( 0.2923287055106771337, 0.07232142847388615958, -0.2123892367102620249 ) ) ;
#2258=CARTESIAN_POINT ( 'NONE',  ( 0.2233192592356400275, 0.3794642856167432798, -0.3073725909049499494 ) ) ;
#2264=FACE_OUTER_BOUND ( 'NONE', #10072, .T. ) ;
#2270=CARTESIAN_POINT ( 'NONE',  ( 0.3613381517857143232, 0.06874999990245758696, -0.1174058825155740587 ) ) ;
#2272=EDGE_CURVE ( 'NONE', #12608, #15982, #20119, .T. ) ;
#2276=FACE_OUTER_BOUND ( 'NONE', #15465, .T. ) ;
#2292=CARTESIAN_POINT ( 'NONE',  ( -0.1534580259519314760, -1.109535145422194601E-16, 0.3483058538587986974 ) ) ;
#2298=CARTESIAN_POINT ( 'NONE',  ( 0.3806690758928571450, 0.4513392855679720372, 0.000000000000000000 ) ) ;
#2308=CARTESIAN_POINT ( 'NONE',  ( -0.3613381517857143232, 0.1008928570453147405, -4.425116109941954795E-17 ) ) ;
#2319=CIRCLE ( 'NONE', #741, 0.3425000000000000266 ) ;
#2324=DIRECTION ( 'NONE',  ( 8.659560562354953812E-17, -0.7071067811865459074, 0.7071067811865492381 ) ) ;
#2326=CARTESIAN_POINT ( 'NONE',  ( 0.3236067977499790249, 0.3267857140906293978, -0.2351141009169892826 ) ) ;
#2334=FACE_OUTER_BOUND ( 'NONE', #3057, .T. ) ;
#2342=FACE_OUTER_BOUND ( 'NONE', #9167, .T. ) ;
#2346=CARTESIAN_POINT ( 'NONE',  ( -0.4000000000000000222, 0.2928571428571427604, -4.898587196589413075E-17 ) ) ;
#2353=CARTESIAN_POINT ( 'NONE',  ( 0.3999999999999999667, 0.2446428569477723525, 0.1299678784931626307 ) ) ;
#2356=CIRCLE ( 'NONE', #1575, 0.3525000000000007017 ) ;
#2368=CIRCLE ( 'NONE', #11329, 0.09499999999999995948 ) ;
#2377=DIRECTION ( 'NONE',  ( 0.000000000000000000, -0.000000000000000000, 1.000000000000000000 ) ) ;
#2378=CARTESIAN_POINT ( 'NONE',  ( 0.3613381517857143232, 0.1366071427596004251, 0.000000000000000000 ) ) ;
#2381=CARTESIAN_POINT ( 'NONE',  ( 0.1116596296178199027, 0.3544642856167432576, 0.3436530038418508792 ) ) ;
#2390=VECTOR ( 'NONE', #14299, 39.37007874015748143 ) ;
#2393=CARTESIAN_POINT ( 'NONE',  ( -0.2923287055106771337, 0.1651785713310290060, -0.2123892367102620804 ) ) ;
#2412=CARTESIAN_POINT ( 'NONE',  ( 0.1355891867880099633, -6.434570819605719236E-16, 0.3400430461746979938 ) ) ;
#2414=CARTESIAN_POINT ( 'NONE',  ( -0.06335377612981410445, 0.3088837756590411265, 0.4000000000000001887 ) ) ;
#2417=DIRECTION ( 'NONE',  ( -0.000000000000000000, -1.000000000000000000, -0.000000000000000000 ) ) ;
#2422=DESIGN_CONTEXT ( 'detailed design', #8883, 'design' ) ;
#2427=CARTESIAN_POINT ( 'NONE',  ( 0.3613381517857143232, -0.009821428668970965531, 0.1174058825155742114 ) ) ;
#2435=CARTESIAN_POINT ( 'NONE',  ( 0.03742218716966667219, 4.101846522467903000E-18, -0.3789181498996747055 ) ) ;
#2438=EDGE_CURVE ( 'NONE', #8827, #15879, #14286, .T. ) ;
#2450=CARTESIAN_POINT ( 'NONE',  ( 0.3613381517857143232, 0.3508928570453146989, 0.000000000000000000 ) ) ;
#2467=EDGE_CURVE ( 'NONE', #7539, #16753, #22901, .T. ) ;
#2468=DIRECTION ( 'NONE',  ( -1.000000000000000000, 0.000000000000000000, -0.000000000000000000 ) ) ;
#2474=CARTESIAN_POINT ( 'NONE',  ( 0.1236067977499789861, 0.3339285712334866263, -0.3804226065180614236 ) ) ;
#2478=VERTEX_POINT ( 'NONE', #20598 ) ;
#2479=DIRECTION ( 'NONE',  ( 0.000000000000000000, 0.000000000000000000, -1.000000000000000000 ) ) ;
#2488=CARTESIAN_POINT ( 'NONE',  ( -7.000945310522701902E-17, 0.4446428569477722803, 0.3999999999999999667 ) ) ;
#2495=CARTESIAN_POINT ( 'NONE',  ( 0.2923287055106771337, 0.1437499999024575981, -0.2123892367102620249 ) ) ;
#2497=EDGE_LOOP ( 'NONE', ( #1375, #11890 ) ) ;
#2506=ORIENTED_EDGE ( 'NONE', *, *, #179, .T. ) ;
#2509=ORIENTED_EDGE ( 'NONE', *, *, #4443, .F. ) ;
#2533=AXIS2_PLACEMENT_3D ( 'NONE', #13434, #7334, #5741 ) ;
#2544=CARTESIAN_POINT ( 'NONE',  ( -0.2233192592356399997, 0.04017857133102901990, 0.3073725909049499494 ) ) ;
#2561=CARTESIAN_POINT ( 'NONE',  ( 4.898587196589413075E-17, 3.700000000000000622, 0.4000000000000000222 ) ) ;
#2584=ADVANCED_FACE ( 'NONE', ( #8501 ), #15825, .F. ) ;
#2591=CARTESIAN_POINT ( 'NONE',  ( 0.2472135954999579721, 0.2589285712334866152, -0.3402603233408159622 ) ) ;
#2593=CARTESIAN_POINT ( 'NONE',  ( 0.000000000000000000, 2.735000000000000320, 0.7500000000000001110 ) ) ;
#2604=CARTESIAN_POINT ( 'NONE',  ( -9.626299801968715084E-16, 0.3464285714285713635, -0.4000000000000000222 ) ) ;
#2613=CARTESIAN_POINT ( 'NONE',  ( 0.2923287055106771337, 0.3580357141881718164, -0.2123892367102620249 ) ) ;
#2616=CARTESIAN_POINT ( 'NONE',  ( -6.979263641208234666E-17, 0.4223214284738860402, 0.3799334167787516980 ) ) ;
#2636=EDGE_CURVE ( 'NONE', #20833, #45, #8068, .T. ) ;
#2662=CARTESIAN_POINT ( 'NONE',  ( 0.3613381517857143232, -0.07767857152611380711, 0.000000000000000000 ) ) ;
#2671=CARTESIAN_POINT ( 'NONE',  ( 0.06791167322627879310, 1.376365001936863736E-16, -0.3730078252257436056 ) ) ;
#2675=DIRECTION ( 'NONE',  ( 0.000000000000000000, 0.000000000000000000, 1.000000000000000000 ) ) ;
#2677=CARTESIAN_POINT ( 'NONE',  ( 0.2994040877653771360, 1.697684548454547126E-17, 0.2026366584349470201 ) ) ;
#2705=CARTESIAN_POINT ( 'NONE',  ( -0.1236067977499790416, 0.2982142855192009279, 0.3804226065180614236 ) ) ;
#2708=LINE ( 'NONE', #19772, #20370 ) ;
#2718=CARTESIAN_POINT ( 'NONE',  ( 9.101228903679513089E-16, 0.3107142857142856096, 0.4000000000000000222 ) ) ;
#2720=ORIENTED_EDGE ( 'NONE', *, *, #14863, .F. ) ;
#2726=CARTESIAN_POINT ( 'NONE',  ( 0.2233192592356399164, 0.3401785713310290227, 0.3073725909049500604 ) ) ;
#2729=CARTESIAN_POINT ( 'NONE',  ( -0.3613381517857143788, 0.3366071427596004084, 0.1174058825155740310 ) ) ;
#2730=AXIS2_PLACEMENT_3D ( 'NONE', #5068, #5189, #1544 ) ;
#2742=CONICAL_SURFACE ( 'NONE', #16383, 0.3125000000000000000, 0.7853981633974482790 ) ;
#2757=DIRECTION ( 'NONE',  ( -0.000000000000000000, -1.000000000000000000, -0.000000000000000000 ) ) ;
#2761=CARTESIAN_POINT ( 'NONE',  ( -0.2977100099089716734, 3.700000000000000622, 0.09499999999999995948 ) ) ;
#2764=EDGE_CURVE ( 'NONE', #13263, #22290, #20047, .T. ) ;
#2774=CARTESIAN_POINT ( 'NONE',  ( 0.2233192592356399997, 0.2901785713310290338, -0.3073725909049500049 ) ) ;
#2782=CARTESIAN_POINT ( 'NONE',  ( 0.3236067977499790249, 0.1214285714285713996, -0.2351141009169892826 ) ) ;
#2805=CARTESIAN_POINT ( 'NONE',  ( 0.3236067977499790249, 0.2642857142857141795, -0.2351141009169892826 ) ) ;
#2818=CARTESIAN_POINT ( 'NONE',  ( 2.326421213736078119E-17, 0.02946428561674332286, -0.3799334167787516425 ) ) ;
#2829=SHAPE_DEFINITION_REPRESENTATION ( #3106, #20236 ) ;
#2839=CARTESIAN_POINT ( 'NONE',  ( 0.1116596296178199860, 0.3651785713310289894, -0.3436530038418508792 ) ) ;
#2846=DIRECTION ( 'NONE',  ( -0.000000000000000000, 1.000000000000000000, -0.000000000000000000 ) ) ;
#2885=CARTESIAN_POINT ( 'NONE',  ( -0.1116596296178199582, 0.3901785713310289561, -0.3436530038418508792 ) ) ;
#2890=CARTESIAN_POINT ( 'NONE',  ( -0.3613381517857144343, 0.3187499999024576147, 0.1174058825155740171 ) ) ;
#2896=CIRCLE ( 'NONE', #12673, 0.7199999999999994182 ) ;
#2927=CARTESIAN_POINT ( 'NONE',  ( 0.3613381517857143232, 0.1544642856167432743, 0.000000000000000000 ) ) ;
#2933=CARTESIAN_POINT ( 'NONE',  ( -0.1236067977499790416, 0.3785714285714284477, 0.3804226065180614236 ) ) ;
#2935=EDGE_LOOP ( 'NONE', ( #4577, #11659, #9443, #16326 ) ) ;
#2938=DIRECTION ( 'NONE',  ( 0.000000000000000000, 1.000000000000000000, 0.000000000000000000 ) ) ;
#2941=CARTESIAN_POINT ( 'NONE',  ( 0.3999999999999999667, 0.4589285712334866263, 0.1299678784931626307 ) ) ;
#2942=VECTOR ( 'NONE', #1534, 39.37007874015748143 ) ;
#2951=CARTESIAN_POINT ( 'NONE',  ( -9.626299801968715084E-16, 0.2660714283763437327, -0.4000000000000000222 ) ) ;
#2953=CONICAL_SURFACE ( 'NONE', #17749, 0.3125000000000000000, 0.7853981633974482790 ) ;
#2966=CARTESIAN_POINT ( 'NONE',  ( -0.3613381517857143232, 0.3866071427596004528, -4.425116109941954795E-17 ) ) ;
#3014=ORIENTED_EDGE ( 'NONE', *, *, #20910, .F. ) ;
#3018=CARTESIAN_POINT ( 'NONE',  ( -6.979263641208234666E-17, 0.4223214284738860402, 0.3799334167787516425 ) ) ;
#3020=CARTESIAN_POINT ( 'NONE',  ( 0.3613381517857143232, 0.2080357141881718774, 0.000000000000000000 ) ) ;
#3027=ORIENTED_EDGE ( 'NONE', *, *, #23214, .F. ) ;
#3037=VERTEX_POINT ( 'NONE', #17851 ) ;
#3041=AXIS2_PLACEMENT_3D ( 'NONE', #529, #771, #15652 ) ;
#3050=CARTESIAN_POINT ( 'NONE',  ( -0.2233192592356399442, 0.03660714275960044034, -0.3073725909049500049 ) ) ;
#3057=EDGE_LOOP ( 'NONE', ( #20706, #20013, #22616, #10692 ) ) ;
#3058=ORIENTED_EDGE ( 'NONE', *, *, #6477, .T. ) ;
#3064=CARTESIAN_POINT ( 'NONE',  ( 0.2233192592356399164, 0.0008928570453147541665, 0.3073725909049500604 ) ) ;
#3090=CARTESIAN_POINT ( 'NONE',  ( 0.1236067977499789861, -0.01428571428571431129, -0.3804226065180614236 ) ) ;
#3099=CARTESIAN_POINT ( 'NONE',  ( -0.3999999999999999667, 0.2089285712334865985, -0.1299678784931626030 ) ) ;
#3102=ORIENTED_EDGE ( 'NONE', *, *, #17350, .T. ) ;
#3106=PRODUCT_DEFINITION_SHAPE ( 'NONE', 'NONE',  #15678 ) ;
#3128=VECTOR ( 'NONE', #2846, 39.37007874015748143 ) ;
#3133=CARTESIAN_POINT ( 'NONE',  ( 2.326421213736078119E-17, 0.3866071427596002308, -0.3799334167787516425 ) ) ;
#3134=CARTESIAN_POINT ( 'NONE',  ( 4.194415287079685308E-17, -2.347681869555226049E-17, -0.3425000000000000266 ) ) ;
#3137=CARTESIAN_POINT ( 'NONE',  ( -0.2923287055106771337, 0.1080357141881718719, 0.2123892367102619971 ) ) ;
#3164=CARTESIAN_POINT ( 'NONE',  ( -0.3613381517857144343, 0.1223214284738861207, 0.1174058825155740171 ) ) ;
#3167=FACE_OUTER_BOUND ( 'NONE', #2935, .T. ) ;
#3168=ADVANCED_FACE ( 'NONE', ( #23673 ), #6867, .T. ) ;
#3178=CARTESIAN_POINT ( 'NONE',  ( -7.726019084026502927E-17, 0.4446428569477723358, 0.4205848896953069405 ) ) ;
#3201=CARTESIAN_POINT ( 'NONE',  ( 0.2472135954999579166, -0.03928571428571429880, 0.3402603233408160732 ) ) ;
#3220=ORIENTED_EDGE ( 'NONE', *, *, #6925, .F. ) ;
#3235=VERTEX_POINT ( 'NONE', #20338 ) ;
#3250=CARTESIAN_POINT ( 'NONE',  ( -0.1116596296178200276, 0.4187499999024575370, 0.3436530038418508792 ) ) ;
#3252=CARTESIAN_POINT ( 'NONE',  ( 0.3613381517857143232, 0.1401785713310289838, -0.1174058825155740587 ) ) ;
#3259=CARTESIAN_POINT ( 'NONE',  ( -7.000945310522701902E-17, 0.2303571426620580065, 0.3999999999999999667 ) ) ;
#3267=CARTESIAN_POINT ( 'NONE',  ( -0.1236067977499789583, 0.2071428571428570731, -0.3804226065180614791 ) ) ;
#3282=CARTESIAN_POINT ( 'NONE',  ( -0.1116596296178199582, -0.03839285724039953607, -0.3436530038418508792 ) ) ;
#3285=CARTESIAN_POINT ( 'NONE',  ( 0.1236067977499789028, 0.01964285694777234345, 0.3804226065180614791 ) ) ;
#3295=CARTESIAN_POINT ( 'NONE',  ( -0.1116596296178199582, 0.1044642856167433131, -0.3436530038418508792 ) ) ;
#3313=EDGE_LOOP ( 'NONE', ( #9399, #16060, #19784, #5093 ) ) ;
#3319=CARTESIAN_POINT ( 'NONE',  ( -0.4000000000000000222, -0.06071428571428573451, 0.1299678784931624920 ) ) ;
#3337=ORIENTED_EDGE ( 'NONE', *, *, #17335, .T. ) ;
#3352=CARTESIAN_POINT ( 'NONE',  ( -0.4000000000000000222, 0.3642857142857142128, -4.898587196589413075E-17 ) ) ;
#3374=CARTESIAN_POINT ( 'NONE',  ( 0.2233192592356399164, 0.3580357141881718164, 0.3073725909049500604 ) ) ;
#3388=AXIS2_PLACEMENT_3D ( 'NONE', #12973, #20390, #7460 ) ;
#3407=CARTESIAN_POINT ( 'NONE',  ( 0.2923287055106771337, -0.05267857152611382654, -0.2123892367102620249 ) ) ;
#3420=CARTESIAN_POINT ( 'NONE',  ( 0.2923287055106771337, 0.2901785713310289783, 0.2123892367102621359 ) ) ;
#3422=FACE_OUTER_BOUND ( 'NONE', #22090, .T. ) ;
#3429=CARTESIAN_POINT ( 'NONE',  ( 0.06335377612981443751, 0.2321876527173024896, 0.4000000000000000222 ) ) ;
#3433=DIRECTION ( 'NONE',  ( -0.000000000000000000, -1.000000000000000000, -0.000000000000000000 ) ) ;
#3441=CARTESIAN_POINT ( 'NONE',  ( 0.2923287055106771337, 0.4151785713310289228, 0.2123892367102621359 ) ) ;
#3459=AXIS2_PLACEMENT_3D ( 'NONE', #7222, #1612, #9409 ) ;
#3464=CARTESIAN_POINT ( 'NONE',  ( 3.827021247335478926E-17, 3.659999999999999698, 0.3125000000000000000 ) ) ;
#3474=CARTESIAN_POINT ( 'NONE',  ( -0.1116596296178199582, 0.1758928570453147100, -0.3436530038418508792 ) ) ;
#3495=PRODUCT ( 'Aloris-BXA-Center-Shaft', 'Aloris-BXA-Center-Shaft', '', ( #8073 ) ) ;
#3507=CARTESIAN_POINT ( 'NONE',  ( 0.1891708636127259202, 2.539511724522405989E-17, 0.3078630284654709781 ) ) ;
#3526=DIRECTION ( 'NONE',  ( 0.000000000000000000, 1.000000000000000000, 0.000000000000000000 ) ) ;
#3528=CARTESIAN_POINT ( 'NONE',  ( 0.3613381517857143232, 0.2973214284738861513, 0.000000000000000000 ) ) ;
#3539=CARTESIAN_POINT ( 'NONE',  ( 0.2233192592356399164, 0.2866071427596003640, 0.3073725909049500604 ) ) ;
#3549=CARTESIAN_POINT ( 'NONE',  ( -9.626299801968715084E-16, 0.2035714285714284866, -0.4000000000000000222 ) ) ;
#3560=CARTESIAN_POINT ( 'NONE',  ( 0.4000000000000000222, -0.1000000000000000056, 0.000000000000000000 ) ) ;
#3566=CARTESIAN_POINT ( 'NONE',  ( 0.1236067977499789028, 0.09107142837634377153, 0.3804226065180614791 ) ) ;
#3592=CARTESIAN_POINT ( 'NONE',  ( 2.326421213736078119E-17, 0.2437499999024575204, -0.3799334167787516980 ) ) ;
#3604=CARTESIAN_POINT ( 'NONE',  ( 0.000000000000000000, 3.700000000000000622, 0.000000000000000000 ) ) ;
#3607=ORIENTED_EDGE ( 'NONE', *, *, #10375, .F. ) ;
#3621=ORIENTED_EDGE ( 'NONE', *, *, #10624, .T. ) ;
#3625=CARTESIAN_POINT ( 'NONE',  ( 0.000000000000000000, 3.669999999999999929, 0.000000000000000000 ) ) ;
#3644=LINE ( 'NONE', #20235, #21852 ) ;
#3646=CARTESIAN_POINT ( 'NONE',  ( 0.2233192592356399164, 0.3580357141881718164, 0.3073725909049500604 ) ) ;
#3648=DIRECTION ( 'NONE',  ( 0.000000000000000000, 1.000000000000000000, 0.000000000000000000 ) ) ;
#3659=CARTESIAN_POINT ( 'NONE',  ( -6.979263641208234666E-17, 0.1366071427596004251, 0.3799334167787516425 ) ) ;
#3664=ORIENTED_EDGE ( 'NONE', *, *, #7956, .F. ) ;
#3672=CARTESIAN_POINT ( 'NONE',  ( 0.4000000000000000222, 0.1857142857142856651, 0.000000000000000000 ) ) ;
#3684=CARTESIAN_POINT ( 'NONE',  ( -0.2472135954999579444, 0.2821428571428570287, -0.3402603233408159622 ) ) ;
#3691=CARTESIAN_POINT ( 'NONE',  ( -0.3236067977499790249, 0.005357142662058073795, 0.2351141009169892271 ) ) ;
#3718=ORIENTED_EDGE ( 'NONE', *, *, #6207, .F. ) ;
#3721=CARTESIAN_POINT ( 'NONE',  ( -0.3613381517857143232, 0.04732142847388616513, -4.425116109941954795E-17 ) ) ;
#3734=CARTESIAN_POINT ( 'NONE',  ( 2.326421213736078119E-17, 0.2258928570453146711, -0.3799334167787516980 ) ) ;
#3745=CARTESIAN_POINT ( 'NONE',  ( 0.2923287055106771337, 0.4151785713310289228, 0.2123892367102621359 ) ) ;
#3764=CARTESIAN_POINT ( 'NONE',  ( 0.000000000000000000, 3.700000000000000622, 0.000000000000000000 ) ) ;
#3765=ORIENTED_EDGE ( 'NONE', *, *, #18070, .T. ) ;
#3772=CARTESIAN_POINT ( 'NONE',  ( 0.3613381517857143232, 0.3651785713310288783, 0.1174058825155742114 ) ) ;
#3775=CARTESIAN_POINT ( 'NONE',  ( -0.2977100099089716734, 3.575000000000000622, -0.09499999999999993172 ) ) ;
#3783=CARTESIAN_POINT ( 'NONE',  ( 0.3613381517857143232, 0.2973214284738861513, 0.000000000000000000 ) ) ;
#3787=CARTESIAN_POINT ( 'NONE',  ( 0.3208197908154664102, -2.427762526784287634E-18, -0.1679480024125937221 ) ) ;
#3793=AXIS2_PLACEMENT_3D ( 'NONE', #10115, #6436, #17540 ) ;
#3807=CARTESIAN_POINT ( 'NONE',  ( -7.726019084026502927E-17, 0.3107142857142856096, 0.4205848896953069405 ) ) ;
#3817=CARTESIAN_POINT ( 'NONE',  ( 2.575339694675500462E-17, 0.1232142855192008835, -0.4205848896953069405 ) ) ;
#3827=ORIENTED_EDGE ( 'NONE', *, *, #18211, .T. ) ;
#3839=CARTESIAN_POINT ( 'NONE',  ( 0.1116596296178199027, -0.02053571438325667992, 0.3436530038418508792 ) ) ;
#3842=CARTESIAN_POINT ( 'NONE',  ( 0.2923287055106771337, 0.01874999990245761194, -0.2123892367102620249 ) ) ;
#3854=ORIENTED_EDGE ( 'NONE', *, *, #2438, .T. ) ;
#3871=CARTESIAN_POINT ( 'NONE',  ( -0.3236067977499790249, 0.4339285712334866041, 0.2351141009169892271 ) ) ;
#3890=CARTESIAN_POINT ( 'NONE',  ( 0.2233192592356399997, 0.3794642856167432798, -0.3073725909049500049 ) ) ;
#3922=ORIENTED_EDGE ( 'NONE', *, *, #1615, .T. ) ;
#3926=CARTESIAN_POINT ( 'NONE',  ( -0.1236067977499790416, 0.2357142857142856818, 0.3804226065180614236 ) ) ;
#3936=CARTESIAN_POINT ( 'NONE',  ( 0.2472135954999579166, 0.09464285694777235802, 0.3402603233408160732 ) ) ;
#3939=CARTESIAN_POINT ( 'NONE',  ( 0.000000000000000000, 3.700000000000000622, 0.000000000000000000 ) ) ;
#3945=VECTOR ( 'NONE', #7374, 39.37007874015748143 ) ;
#3955=CARTESIAN_POINT ( 'NONE',  ( -0.3613381517857143232, -0.04553571438325666049, -0.1174058825155741004 ) ) ;
#3959=CARTESIAN_POINT ( 'NONE',  ( 0.3613381517857143232, 0.1508928570453147155, 0.1174058825155741975 ) ) ;
#3970=CARTESIAN_POINT ( 'NONE',  ( 0.2233192592356399164, 0.1258928570453146933, 0.3073725909049500604 ) ) ;
#3997=ORIENTED_EDGE ( 'NONE', *, *, #2272, .F. ) ;
#4001=VECTOR ( 'NONE', #17256, 39.37007874015748143 ) ;
#4010=CARTESIAN_POINT ( 'NONE',  ( 0.2233192592356399997, 0.3080357141881718275, -0.3073725909049500049 ) ) ;
#4040=CARTESIAN_POINT ( 'NONE',  ( -0.4000000000000000222, 0.1499999999999999667, -4.898587196589413075E-17 ) ) ;
#4047=CARTESIAN_POINT ( 'NONE',  ( 0.1236067977499789028, 0.3767857140906294422, 0.3804226065180614791 ) ) ;
#4069=CARTESIAN_POINT ( 'NONE',  ( 2.326421213736078119E-17, 0.01160714275960046671, -0.3799334167787516425 ) ) ;
#4072=CARTESIAN_POINT ( 'NONE',  ( -0.2923287055106771337, 0.3401785713310290227, 0.2123892367102619971 ) ) ;
#4089=DIRECTION ( 'NONE',  ( 0.000000000000000000, 1.000000000000000000, 0.000000000000000000 ) ) ;
#4102=CARTESIAN_POINT ( 'NONE',  ( -0.4000000000000000222, 0.4303571426620579898, 0.1299678784931624920 ) ) ;
#4109=ADVANCED_FACE ( 'NONE', ( #14410 ), #12118, .T. ) ;
#4126=CARTESIAN_POINT ( 'NONE',  ( -0.3613381517857143232, 0.4044642856167432465, -4.425116109941954795E-17 ) ) ;
#4133=CARTESIAN_POINT ( 'NONE',  ( 0.4000000000000000222, 0.1053571426620580481, 0.000000000000000000 ) ) ;
#4142=EDGE_LOOP ( 'NONE', ( #4379, #6293, #19773, #5680 ) ) ;
#4143=CARTESIAN_POINT ( 'NONE',  ( 0.3999999999999999667, 0.3232142855192008946, -0.1299678784931625197 ) ) ;
#4147=CARTESIAN_POINT ( 'NONE',  ( -0.3613381517857143232, 0.3830357141881717276, -0.1174058825155741143 ) ) ;
#4149=LINE ( 'NONE', #18665, #7249 ) ;
#4161=CARTESIAN_POINT ( 'NONE',  ( -0.1236067977499790416, 0.01249999980491520342, 0.3804226065180614236 ) ) ;
#4162=CARTESIAN_POINT ( 'NONE',  ( 0.4000000000000000222, 0.2571428571428571175, 0.000000000000000000 ) ) ;
#4170=CARTESIAN_POINT ( 'NONE',  ( -0.4000000000000000222, 0.2160714283763437438, 0.1299678784931624920 ) ) ;
#4182=CARTESIAN_POINT ( 'NONE',  ( 0.2472135954999579166, 0.3178571428571427826, 0.3402603233408160732 ) ) ;
#4192=CARTESIAN_POINT ( 'NONE',  ( 0.3613381517857143232, -0.006250000097542392913, 0.000000000000000000 ) ) ;
#4195=CARTESIAN_POINT ( 'NONE',  ( 0.2233192592356400275, 0.3080357141881718275, -0.3073725909049499494 ) ) ;
#4205=VERTEX_POINT ( 'NONE', #16477 ) ;
#4207=CIRCLE ( 'NONE', #3041, 0.3525000000000007017 ) ;
#4209=CARTESIAN_POINT ( 'NONE',  ( -0.1116596296178199582, 0.1580357141881718608, -0.3436530038418508792 ) ) ;
#4226=CARTESIAN_POINT ( 'NONE',  ( -0.4000000000000000222, 0.4267857140906294311, -4.898587196589413075E-17 ) ) ;
#4231=CARTESIAN_POINT ( 'NONE',  ( -0.2733612579097375317, -3.892158461848095304E-18, 0.2765269779737352662 ) ) ;
#4234=CARTESIAN_POINT ( 'NONE',  ( -0.1236067977499789583, 0.2785714285714285254, -0.3804226065180614791 ) ) ;
#4245=ADVANCED_FACE ( 'NONE', ( #3422 ), #7208, .F. ) ;
#4248=CARTESIAN_POINT ( 'NONE',  ( 0.1116596296178199860, -0.06339285724039953052, -0.3436530038418508792 ) ) ;
#4256=DIRECTION ( 'NONE',  ( -0.000000000000000000, -1.000000000000000000, -0.000000000000000000 ) ) ;
#4257=CARTESIAN_POINT ( 'NONE',  ( -0.2316346313134401980, -9.420544349976220987E-18, -0.3200023620661306412 ) ) ;
#4269=CARTESIAN_POINT ( 'NONE',  ( 0.3613381517857143232, 0.4223214284738860957, 0.000000000000000000 ) ) ;
#4277=CARTESIAN_POINT ( 'NONE',  ( 0.3116633497045768197, 3.673292956572201451, 0.09499999999999995948 ) ) ;
#4280=CARTESIAN_POINT ( 'NONE',  ( -0.2472135954999579999, 0.3660714283763437105, 0.3402603233408160732 ) ) ;
#4281=CARTESIAN_POINT ( 'NONE',  ( 0.3236067977499790249, 0.3357142857142856318, -0.2351141009169892826 ) ) ;
#4284=DIRECTION ( 'NONE',  ( 0.000000000000000000, 0.000000000000000000, -1.000000000000000000 ) ) ;
#4288=CARTESIAN_POINT ( 'NONE',  ( -0.3999999999999999667, 0.2803571426620579676, -0.1299678784931626030 ) ) ;
#4294=CARTESIAN_POINT ( 'NONE',  ( -0.4749999999999999778, 3.575000000000000622, -0.09499999999999995948 ) ) ;
#4309=CARTESIAN_POINT ( 'NONE',  ( -0.1116596296178199582, 0.08660714275960045005, -0.3436530038418508792 ) ) ;
#4312=EDGE_LOOP ( 'NONE', ( #13864, #136, #23651, #2183, #17958, #11924, #9463, #3827, #10888, #9531, #3058, #21900, #9516, #22950, #4621 ) ) ;
#4313=CARTESIAN_POINT ( 'NONE',  ( -0.1116596296178199582, 0.3901785713310289561, -0.3436530038418508792 ) ) ;
#4317=CARTESIAN_POINT ( 'NONE',  ( -0.4749999999999999778, 3.700000000000000622, -0.09499999999999995948 ) ) ;
#4325=CARTESIAN_POINT ( 'NONE',  ( -0.2923287055106771337, 0.3080357141881718275, -0.2123892367102620804 ) ) ;
#4327=ORIENTED_EDGE ( 'NONE', *, *, #11390, .F. ) ;
#4329=ORIENTED_EDGE ( 'NONE', *, *, #4662, .F. ) ;
#4335=DIRECTION ( 'NONE',  ( -0.000000000000000000, -1.000000000000000000, -0.000000000000000000 ) ) ;
#4346=CARTESIAN_POINT ( 'NONE',  ( -0.4749999999999999778, 3.700000000000000622, 0.09499999999999995948 ) ) ;
#4351=CARTESIAN_POINT ( 'NONE',  ( -0.3394572874457115752, 3.700000000000000622, 0.09499999999999993172 ) ) ;
#4353=DIRECTION ( 'NONE',  ( 0.000000000000000000, 0.000000000000000000, 1.000000000000000000 ) ) ;
#4355=ADVANCED_FACE ( 'NONE', ( #5735 ), #9665, .T. ) ;
#4358=ADVANCED_FACE ( 'NONE', ( #2073 ), #13563, .T. ) ;
#4363=CARTESIAN_POINT ( 'NONE',  ( -0.1116596296178200276, -0.02767857152611381821, 0.3436530038418508792 ) ) ;
#4370=CARTESIAN_POINT ( 'NONE',  ( -0.4749999999999999778, 3.575000000000000622, 0.09499999999999995948 ) ) ;
#4372=CARTESIAN_POINT ( 'NONE',  ( 0.1272547916512738186, -3.800488706749810574E-17, -0.3527189223800989981 ) ) ;
#4379=ORIENTED_EDGE ( 'NONE', *, *, #8802, .F. ) ;
#4381=VERTEX_POINT ( 'NONE', #15605 ) ;
#4398=CARTESIAN_POINT ( 'NONE',  ( -0.3236067977499790249, 0.1571428571428570564, 0.2351141009169892271 ) ) ;
#4402=CARTESIAN_POINT ( 'NONE',  ( 0.000000000000000000, 3.700000000000000622, 0.000000000000000000 ) ) ;
#4408=CARTESIAN_POINT ( 'NONE',  ( 0.2472135954999579166, 0.3803571426620580564, 0.3402603233408160732 ) ) ;
#4417=ADVANCED_FACE ( 'NONE', ( #603 ), #19254, .T. ) ;
#4427=CARTESIAN_POINT ( 'NONE',  ( 4.898587196589413075E-17, 3.700000000000000622, 0.4000000000000000222 ) ) ;
#4428=CARTESIAN_POINT ( 'NONE',  ( -0.1116596296178200276, 0.2580357141881718941, 0.3436530038418508792 ) ) ;
#4431=CARTESIAN_POINT ( 'NONE',  ( 0.3613381517857143232, 0.2937499999024575370, 0.1174058825155741975 ) ) ;
#4442=CARTESIAN_POINT ( 'NONE',  ( -0.1116596296178200276, 0.2580357141881718941, 0.3436530038418508792 ) ) ;
#4443=EDGE_CURVE ( 'NONE', #18346, #4780, #10829, .T. ) ;
#4462=CARTESIAN_POINT ( 'NONE',  ( 4.898587196589413075E-17, 3.700000000000000622, 0.4000000000000000222 ) ) ;
#4483=CARTESIAN_POINT ( 'NONE',  ( -0.2923287055106771337, 0.09374999990245758141, -0.2123892367102620804 ) ) ;
#4486=CARTESIAN_POINT ( 'NONE',  ( 0.3613381517857143232, 0.01160714275960046671, 0.000000000000000000 ) ) ;
#4488=DIRECTION ( 'NONE',  ( 0.000000000000000000, 0.000000000000000000, 1.000000000000000000 ) ) ;
#4489=ORIENTED_EDGE ( 'NONE', *, *, #14723, .T. ) ;
#4509=CARTESIAN_POINT ( 'NONE',  ( -0.2977100099089716734, 3.575000000000000622, 0.09499999999999993172 ) ) ;
#4523=CARTESIAN_POINT ( 'NONE',  ( -0.3999999999999999667, 0.3607142857142855430, -0.1299678784931626030 ) ) ;
#4525=EDGE_LOOP ( 'NONE', ( #7726, #6936, #17713, #19332, #19944 ) ) ;
#4531=CARTESIAN_POINT ( 'NONE',  ( 0.3999999999999999667, 0.2517857140906293867, -0.1299678784931625475 ) ) ;
#4550=CARTESIAN_POINT ( 'NONE',  ( -0.1236067977499790416, 0.02142857142857140795, 0.3804226065180614236 ) ) ;
#4553=CARTESIAN_POINT ( 'NONE',  ( -0.2923287055106771337, 0.2508928570453147211, 0.2123892367102619971 ) ) ;
#4556=CARTESIAN_POINT ( 'NONE',  ( -0.3613381517857143232, 0.3330357141881718497, -4.425116109941954795E-17 ) ) ;
#4577=ORIENTED_EDGE ( 'NONE', *, *, #7239, .F. ) ;
#4586=DIRECTION ( 'NONE',  ( 0.000000000000000000, -0.000000000000000000, 1.000000000000000000 ) ) ;
#4589=CARTESIAN_POINT ( 'NONE',  ( 3.827021247335478926E-17, 3.700000000000000622, 0.3125000000000000000 ) ) ;
#4605=CARTESIAN_POINT ( 'NONE',  ( 2.326421213736078119E-17, 0.2973214284738861513, -0.3799334167787516425 ) ) ;
#4611=ORIENTED_EDGE ( 'NONE', *, *, #8462, .F. ) ;
#4621=ORIENTED_EDGE ( 'NONE', *, *, #15666, .F. ) ;
#4633=( BOUNDED_CURVE ( )  B_SPLINE_CURVE ( 2, ( #22557, #483, #19027, #20968, #9514, #22675, #9397, #5849, #22313, #16948, #5611, #11596, #247 ),
 .UNSPECIFIED., .F., .T. ) 
 B_SPLINE_CURVE_WITH_KNOTS ( ( 3, 2, 2, 2, 2, 2, 3 ),
 ( 0.8214285714285715079, 0.8285714285714286254, 0.8428571428571428603, 0.8571428571428570953, 0.8714285714285714413, 0.8857142857142856762, 0.8928571428571429047 ),
 .UNSPECIFIED. ) 
 CURVE ( )  GEOMETRIC_REPRESENTATION_ITEM ( )  RATIONAL_B_SPLINE_CURVE ( ( 0.9755282581475768211, 0.9755282581475769321, 1.000000000000000000, 0.9510565162951535312, 1.000000000000000000, 0.9510565162951535312, 1.000000000000000000, 0.9510565162951535312, 1.000000000000000000, 0.9510565162951535312, 1.000000000000000000, 0.9755282581475765991, 0.9755282581475768211 ) ) 
 REPRESENTATION_ITEM ( '' )  );
#4636=CARTESIAN_POINT ( 'NONE',  ( 0.3236067977499789694, 0.2499999999999999167, 0.2351141009169893659 ) ) ;
#4648=CARTESIAN_POINT ( 'NONE',  ( -0.3613381517857144343, 0.1223214284738861624, 0.1174058825155740171 ) ) ;
#4661=VERTEX_POINT ( 'NONE', #6687 ) ;
#4662=EDGE_CURVE ( 'NONE', #3037, #23444, #14132, .T. ) ;
#4665=ORIENTED_EDGE ( 'NONE', *, *, #2764, .T. ) ;
#4671=CARTESIAN_POINT ( 'NONE',  ( -0.3613381517857143232, 0.2437499999024575481, -4.425116109941954795E-17 ) ) ;
#4700=LINE ( 'NONE', #4462, #17111 ) ;
#4718=CARTESIAN_POINT ( 'NONE',  ( -0.1116596296178200276, 0.3294642856167432354, 0.3436530038418508792 ) ) ;
#4748=CARTESIAN_POINT ( 'NONE',  ( 0.3613381517857143232, 0.07946428561674329094, 0.1174058825155742114 ) ) ;
#4752=CARTESIAN_POINT ( 'NONE',  ( -0.1236067977499789583, 0.1357142857142856485, -0.3804226065180614791 ) ) ;
#4757=DIRECTION ( 'NONE',  ( -0.000000000000000000, -1.000000000000000000, -0.000000000000000000 ) ) ;
#4760=CARTESIAN_POINT ( 'NONE',  ( -0.2923287055106771337, -0.03125000009754238389, -0.2123892367102620804 ) ) ;
#4766=ORIENTED_EDGE ( 'NONE', *, *, #1482, .F. ) ;
#4772=ORIENTED_EDGE ( 'NONE', *, *, #20735, .T. ) ;
#4773=( BOUNDED_CURVE ( )  B_SPLINE_CURVE ( 2, ( #1391, #16269, #14445, #15784, #12626, #3099, #17979, #14076, #21630, #4795, #20043, #14196, #1149 ),
 .UNSPECIFIED., .F., .T. ) 
 B_SPLINE_CURVE_WITH_KNOTS ( ( 3, 2, 2, 2, 2, 2, 3 ),
 ( 0.4642857142857143016, 0.4714285714285714191, 0.4857142857142857095, 0.5000000000000000000, 0.5142857142857142350, 0.5285714285714285809, 0.5357142857142856984 ),
 .UNSPECIFIED. ) 
 CURVE ( )  GEOMETRIC_REPRESENTATION_ITEM ( )  RATIONAL_B_SPLINE_CURVE ( ( 0.9755282581475767101, 0.9755282581475768211, 1.000000000000000000, 0.9510565162951535312, 1.000000000000000000, 0.9510565162951535312, 1.000000000000000000, 0.9510565162951535312, 1.000000000000000000, 0.9510565162951535312, 1.000000000000000000, 0.9755282581475768211, 0.9755282581475768211 ) ) 
 REPRESENTATION_ITEM ( '' )  );
#4780=VERTEX_POINT ( 'NONE', #6811 ) ;
#4785=CARTESIAN_POINT ( 'NONE',  ( -0.1116596296178199582, 0.3008928570453147100, -0.3436530038418508792 ) ) ;
#4795=CARTESIAN_POINT ( 'NONE',  ( -0.2472135954999579999, 0.2232142855192008613, 0.3402603233408160732 ) ) ;
#4802=EDGE_LOOP ( 'NONE', ( #3922, #9926, #16449, #9587 ) ) ;
#4814=PLANE ( 'NONE',  #15587 ) ;
#4819=CARTESIAN_POINT ( 'NONE',  ( -7.000945310522701902E-17, 0.3821428571428570620, 0.3999999999999999667 ) ) ;
#4833=CARTESIAN_POINT ( 'NONE',  ( -0.1116596296178200276, 0.3473214284738860846, 0.3436530038418508792 ) ) ;
#4836=CARTESIAN_POINT ( 'NONE',  ( 0.1116596296178199860, 0.2223214284738861402, -0.3436530038418508792 ) ) ;
#4838=EDGE_CURVE ( 'NONE', #13969, #4661, #8495, .T. ) ;
#4846=CARTESIAN_POINT ( 'NONE',  ( 0.06335377612981431261, 0.1303123470876126344, -0.4000000000000000777 ) ) ;
#4853=CARTESIAN_POINT ( 'NONE',  ( 4.898587196589413075E-17, 3.700000000000000622, 0.4000000000000000222 ) ) ;
#4860=CARTESIAN_POINT ( 'NONE',  ( -0.2923287055106771337, 0.02232142847388617762, -0.2123892367102620804 ) ) ;
#4872=CARTESIAN_POINT ( 'NONE',  ( 2.326421213736078119E-17, 0.02946428561674331245, -0.3799334167787516425 ) ) ;
#4880=EDGE_LOOP ( 'NONE', ( #17383, #1045, #8185, #8434, #11084, #11761, #6330, #10754 ) ) ;
#4885=CARTESIAN_POINT ( 'NONE',  ( 0.2472135954999579166, 0.4517857140906294533, 0.3402603233408160732 ) ) ;
#4911=CARTESIAN_POINT ( 'NONE',  ( -0.2923287055106771337, 0.1651785713310290060, -0.2123892367102620804 ) ) ;
#4940=DIRECTION ( 'NONE',  ( 0.000000000000000000, 0.000000000000000000, 1.000000000000000000 ) ) ;
#4956=DIRECTION ( 'NONE',  ( 0.000000000000000000, -0.000000000000000000, 1.000000000000000000 ) ) ;
#4958=CARTESIAN_POINT ( 'NONE',  ( -0.1116596296178199582, 0.1580357141881718608, -0.3436530038418508792 ) ) ;
#4961=CARTESIAN_POINT ( 'NONE',  ( 0.3613381517857143232, 0.2223214284738861402, 0.1174058825155741975 ) ) ;
#4975=EDGE_CURVE ( 'NONE', #5171, #9466, #15602, .T. ) ;
#4978=EDGE_CURVE ( 'NONE', #3235, #20999, #11620, .T. ) ;
#4989=CARTESIAN_POINT ( 'NONE',  ( 0.2233192592356399997, -0.04910714295468525392, -0.3073725909049500049 ) ) ;
#5003=CARTESIAN_POINT ( 'NONE',  ( -0.3613381517857143232, 0.04732142847388616513, -4.425116109941954795E-17 ) ) ;
#5013=CARTESIAN_POINT ( 'NONE',  ( 0.1236067977499789861, 0.2624999998049151739, -0.3804226065180614236 ) ) ;
#5020=ORIENTED_EDGE ( 'NONE', *, *, #17624, .T. ) ;
#5026=CARTESIAN_POINT ( 'NONE',  ( -0.3236067977499790249, 0.01428571428571426098, 0.2351141009169892271 ) ) ;
#5055=ORIENTED_EDGE ( 'NONE', *, *, #6477, .F. ) ;
#5065=AXIS2_PLACEMENT_3D ( 'NONE', #19638, #2938, #17938 ) ;
#5068=CARTESIAN_POINT ( 'NONE',  ( -0.4749999999999999778, 3.575000000000000622, 2.908536147974962357E-17 ) ) ;
#5076=CARTESIAN_POINT ( 'NONE',  ( 0.3613381517857143232, 0.2044642856167432632, 0.1174058825155742114 ) ) ;
#5084=CARTESIAN_POINT ( 'NONE',  ( -4.638126268221291196E-16, 0.1321428571428571175, -0.4000000000000000222 ) ) ;
#5093=ORIENTED_EDGE ( 'NONE', *, *, #11572, .F. ) ;
#5106=DIRECTION ( 'NONE',  ( 0.000000000000000000, 0.000000000000000000, -1.000000000000000000 ) ) ;
#5107=CARTESIAN_POINT ( 'NONE',  ( -0.2233192592356399997, -0.01339285724039954162, 0.3073725909049499494 ) ) ;
#5116=EDGE_CURVE ( 'NONE', #7566, #2478, #4207, .T. ) ;
#5121=CARTESIAN_POINT ( 'NONE',  ( 0.3613381517857143232, 0.08303571418817189131, 0.000000000000000000 ) ) ;
#5145=CARTESIAN_POINT ( 'NONE',  ( -6.979263641208234666E-17, 0.4044642856167431355, 0.3799334167787516425 ) ) ;
#5153=FACE_OUTER_BOUND ( 'NONE', #10, .T. ) ;
#5162=ADVANCED_FACE ( 'NONE', ( #11667 ), #18243, .T. ) ;
#5171=VERTEX_POINT ( 'NONE', #21284 ) ;
#5189=DIRECTION ( 'NONE',  ( 0.000000000000000000, 1.000000000000000000, 0.000000000000000000 ) ) ;
#5192=CONICAL_SURFACE ( 'NONE', #23878, 0.7199999999999994182, 0.7853981633974506105 ) ;
#5194=CARTESIAN_POINT ( 'NONE',  ( 0.1116596296178199860, 0.3830357141881718386, -0.3436530038418508792 ) ) ;
#5196=CARTESIAN_POINT ( 'NONE',  ( -0.1116596296178200276, 0.4008928570453146878, 0.3436530038418508792 ) ) ;
#5206=CARTESIAN_POINT ( 'NONE',  ( 1.750236327630675475E-17, 0.05178571409062948661, -0.3999999999999999667 ) ) ;
#5211=CARTESIAN_POINT ( 'NONE',  ( -0.4000000000000000222, 0.2214285714285713358, -4.898587196589413075E-17 ) ) ;
#5227=CARTESIAN_POINT ( 'NONE',  ( 0.2233192592356399997, 0.02232142847388616722, -0.3073725909049500049 ) ) ;
#5230=CARTESIAN_POINT ( 'NONE',  ( 4.375590819076689459E-17, 0.01607142837634377430, 0.4000000000000000222 ) ) ;
#5242=CARTESIAN_POINT ( 'NONE',  ( 0.3613381517857143232, 0.1580357141881718608, -0.1174058825155740587 ) ) ;
#5245=DIRECTION ( 'NONE',  ( 0.000000000000000000, 1.000000000000000000, 0.000000000000000000 ) ) ;
#5247=VERTEX_POINT ( 'NONE', #19207 ) ;
#5251=CIRCLE ( 'NONE', #19263, 0.4000000000000000222 ) ;
#5267=CARTESIAN_POINT ( 'NONE',  ( 0.1236067977499789028, 0.02857142857142853584, 0.3804226065180614791 ) ) ;
#5271=PLANE ( 'NONE',  #11300 ) ;
#5291=ADVANCED_FACE ( 'NONE', ( #2276 ), #10071, .F. ) ;
#5293=B_SPLINE_CURVE_WITH_KNOTS ( 'NONE', 3,
 ( #3507, #7295, #2412, #11930, #19349, #21177, #8239, #13523, #6175, #18994, #11440, #453, #2292, #20938, #9727, #4231, #7771, #17517, #331, #17401, #20818, #17282, #694, #11683, #18871, #6056 ),
 .UNSPECIFIED., .F., .F.,
 ( 4, 2, 2, 2, 2, 2, 2, 2, 2, 2, 2, 2, 4 ),
 ( 0.000000000000000000, 0.002376276648075994861, 0.004752553296151989723, 0.005940691620189986720, 0.007128829944227983717, 0.008316968268265981581, 0.009505106592303981181, 0.01188138324037997691, 0.01425765988845596743, 0.01544579821249396356, 0.01663393653653195969, 0.01782207486056995235, 0.01901021318460794501 ),
 .UNSPECIFIED. ) ;
#5325=CARTESIAN_POINT ( 'NONE',  ( -4.638126268221291196E-16, 0.06071428571428570675, -0.4000000000000000222 ) ) ;
#5354=CARTESIAN_POINT ( 'NONE',  ( 0.1116596296178199860, 0.2401785713310289616, -0.3436530038418508792 ) ) ;
#5367=CARTESIAN_POINT ( 'NONE',  ( -6.979263641208234666E-17, 0.2794642856167432465, 0.3799334167787516425 ) ) ;
#5378=CARTESIAN_POINT ( 'NONE',  ( 0.2472135954999579721, 0.1964285714285713969, -0.3402603233408160732 ) ) ;
#5391=CARTESIAN_POINT ( 'NONE',  ( 0.1236067977499789028, -0.04285714285714287142, 0.3804226065180614791 ) ) ;
#5397=CARTESIAN_POINT ( 'NONE',  ( -7.726019084026502927E-17, 0.1589285712334866651, 0.4205848896953069405 ) ) ;
#5425=CARTESIAN_POINT ( 'NONE',  ( -0.2923287055106771337, 0.04017857133102904071, -0.2123892367102620804 ) ) ;
#5442=VECTOR ( 'NONE', #1270, 39.37007874015748143 ) ;
#5455=CARTESIAN_POINT ( 'NONE',  ( -0.2472135954999579444, 0.05892857123348661103, -0.3402603233408160732 ) ) ;
#5475=AXIS2_PLACEMENT_3D ( 'NONE', #6227, #21350, #19633 ) ;
#5479=CARTESIAN_POINT ( 'NONE',  ( 2.326421213736078119E-17, 0.1723214284738861513, -0.3799334167787516425 ) ) ;
#5490=CARTESIAN_POINT ( 'NONE',  ( 0.1116596296178199860, 0.2401785713310289616, -0.3436530038418508792 ) ) ;
#5513=CARTESIAN_POINT ( 'NONE',  ( 0.3236067977499790249, -0.02142857142857144265, -0.2351141009169892826 ) ) ;
#5516=FACE_OUTER_BOUND ( 'NONE', #909, .T. ) ;
#5520=CARTESIAN_POINT ( 'NONE',  ( 0.4000000000000000222, 0.03392857123348664433, 0.000000000000000000 ) ) ;
#5545=CARTESIAN_POINT ( 'NONE',  ( -0.2233192592356400275, 0.1294642856167432798, 0.3073725909049499494 ) ) ;
#5558=CARTESIAN_POINT ( 'NONE',  ( 0.2233192592356400275, 0.2187499999024575814, -0.3073725909049499494 ) ) ;
#5568=CARTESIAN_POINT ( 'NONE',  ( 0.1116596296178199027, 0.3366071427596004084, 0.3436530038418508792 ) ) ;
#5594=CARTESIAN_POINT ( 'NONE',  ( -0.2233192592356399997, 0.2723214284738861291, 0.3073725909049499494 ) ) ;
#5603=CARTESIAN_POINT ( 'NONE',  ( 0.000000000000000000, 2.735000000000000320, 0.000000000000000000 ) ) ;
#5607=CARTESIAN_POINT ( 'NONE',  ( 0.3613381517857143232, 0.2258928570453146989, 0.000000000000000000 ) ) ;
#5611=CARTESIAN_POINT ( 'NONE',  ( 0.1236067977499789861, 0.4053571426620580787, -0.3804226065180614236 ) ) ;
#5618=VECTOR ( 'NONE', #809, 39.37007874015748143 ) ;
#5632=CARTESIAN_POINT ( 'NONE',  ( -0.06335377612981453466, 0.01424091832109927562, 0.3999999999999999667 ) ) ;
#5633=CARTESIAN_POINT ( 'NONE',  ( 0.2472135954999579721, 0.1964285714285713969, -0.3402603233408159622 ) ) ;
#5641=CARTESIAN_POINT ( 'NONE',  ( -0.3236067977499789694, -0.008928571623656208003, -0.2351141009169893104 ) ) ;
#5642=CARTESIAN_POINT ( 'NONE',  ( 0.000000000000000000, 3.669999999999999929, 0.7500000000000001110 ) ) ;
#5656=VECTOR ( 'NONE', #10671, 39.37007874015748143 ) ;
#5664=CARTESIAN_POINT ( 'NONE',  ( 0.2233192592356399164, 0.05446428561674330343, 0.3073725909049500604 ) ) ;
#5668=CARTESIAN_POINT ( 'NONE',  ( -0.2923287055106771337, 0.1830357141881718552, -0.2123892367102620804 ) ) ;
#5680=ORIENTED_EDGE ( 'NONE', *, *, #6985, .F. ) ;
#5681=CARTESIAN_POINT ( 'NONE',  ( 0.2923287055106771337, 0.07232142847388615958, -0.2123892367102620249 ) ) ;
#5699=CARTESIAN_POINT ( 'NONE',  ( -0.1236067977499790416, 0.08392857123348662629, 0.3804226065180614236 ) ) ;
#5709=VECTOR ( 'NONE', #8684, 39.37007874015748143 ) ;
#5714=( BOUNDED_CURVE ( )  B_SPLINE_CURVE ( 2, ( #13431, #2209, #22439, #15017, #365, #7807, #20852, #4143, #2326, #17200, #13313, #485, #13558 ),
 .UNSPECIFIED., .F., .F. ) 
 B_SPLINE_CURVE_WITH_KNOTS ( ( 3, 2, 2, 2, 2, 2, 3 ),
 ( 0.6785714285714286031, 0.6857142857142857206, 0.6999999999999999556, 0.7142857142857143016, 0.7285714285714285365, 0.7428571428571428825, 0.7500000000000000000 ),
 .UNSPECIFIED. ) 
 CURVE ( )  GEOMETRIC_REPRESENTATION_ITEM ( )  RATIONAL_B_SPLINE_CURVE ( ( 0.9755282581475768211, 0.9755282581475769321, 1.000000000000000000, 0.9510565162951535312, 1.000000000000000000, 0.9510565162951535312, 1.000000000000000000, 0.9510565162951535312, 1.000000000000000000, 0.9510565162951535312, 1.000000000000000000, 0.9755282581475768211, 0.9755282581475768211 ) ) 
 REPRESENTATION_ITEM ( '' )  );
#5722=CARTESIAN_POINT ( 'NONE',  ( -0.2923287055106771337, 0.2544642856167432798, -0.2123892367102620804 ) ) ;
#5725=DIRECTION ( 'NONE',  ( 0.000000000000000000, 0.000000000000000000, 1.000000000000000000 ) ) ;
#5735=FACE_OUTER_BOUND ( 'NONE', #13772, .T. ) ;
#5741=DIRECTION ( 'NONE',  ( 0.000000000000000000, 0.000000000000000000, 1.000000000000000000 ) ) ;
#5756=CARTESIAN_POINT ( 'NONE',  ( -0.3236067977499790249, 0.2999999999999999334, 0.2351141009169892271 ) ) ;
#5763=AXIS2_PLACEMENT_3D ( 'NONE', #18777, #14247, #12836 ) ;
#5764=CARTESIAN_POINT ( 'NONE',  ( -7.726019084026502927E-17, 0.01607142837634378124, 0.4205848896953069405 ) ) ;
#5770=CARTESIAN_POINT ( 'NONE',  ( -0.4000000000000000222, 0.2874999998049151406, 0.1299678784931624920 ) ) ;
#5782=CARTESIAN_POINT ( 'NONE',  ( -0.3613381517857143232, -0.04196428581182810175, -4.425116109941954795E-17 ) ) ;
#5785=CARTESIAN_POINT ( 'NONE',  ( -0.3613381517857143788, 0.1937499999024576425, 0.1174058825155740310 ) ) ;
#5799=CARTESIAN_POINT ( 'NONE',  ( 0.3613381517857143232, 0.2044642856167432909, 0.1174058825155741975 ) ) ;
#5819=CARTESIAN_POINT ( 'NONE',  ( -0.1236067977499790416, 0.3071428571428570509, 0.3804226065180614236 ) ) ;
#5835=CARTESIAN_POINT ( 'NONE',  ( 0.3613381517857143232, 0.3008928570453147100, -0.1174058825155740587 ) ) ;
#5843=CARTESIAN_POINT ( 'NONE',  ( 0.06335377612981431261, 0.1213837754639564281, -0.4000000000000000777 ) ) ;
#5849=CARTESIAN_POINT ( 'NONE',  ( 0.3999999999999999667, 0.3946428569477721804, -0.1299678784931625197 ) ) ;
#5865=DIRECTION ( 'NONE',  ( 0.000000000000000000, 0.000000000000000000, 1.000000000000000000 ) ) ;
#5867=CARTESIAN_POINT ( 'NONE',  ( 0.2472135954999579166, 0.1749999999999999889, 0.3402603233408160732 ) ) ;
#5874=CARTESIAN_POINT ( 'NONE',  ( -0.2472135954999579999, 0.1517857140906294644, 0.3402603233408159622 ) ) ;
#5899=CARTESIAN_POINT ( 'NONE',  ( 0.3613381517857143232, 0.06517857133102902822, 0.000000000000000000 ) ) ;
#5902=CARTESIAN_POINT ( 'NONE',  ( 0.1116596296178199027, 0.2830357141881718053, 0.3436530038418508792 ) ) ;
#5915=CARTESIAN_POINT ( 'NONE',  ( 0.2233192592356399164, 0.05446428561674330343, 0.3073725909049500604 ) ) ;
#5933=EDGE_CURVE ( 'NONE', #5247, #1426, #21371, .T. ) ;
#5943=VERTEX_POINT ( 'NONE', #18432 ) ;
#5952=CARTESIAN_POINT ( 'NONE',  ( 0.2923287055106771337, 0.0008928570453147542749, -0.2123892367102620249 ) ) ;
#5970=CARTESIAN_POINT ( 'NONE',  ( 0.2923287055106771337, 0.3580357141881718164, -0.2123892367102620249 ) ) ;
#5981=CARTESIAN_POINT ( 'NONE',  ( 1.750236327630675475E-17, 0.2749999999999999112, -0.3999999999999999667 ) ) ;
#5985=CARTESIAN_POINT ( 'NONE',  ( -0.3999999999999999667, 0.3517857140906294200, -0.1299678784931626030 ) ) ;
#5986=CARTESIAN_POINT ( 'NONE',  ( -0.3999999999999999667, 0.2178571428571427493, -0.1299678784931626030 ) ) ;
#5993=CARTESIAN_POINT ( 'NONE',  ( -0.3999999999999999667, 0.4232142855192008724, -0.1299678784931626030 ) ) ;
#6001=ORIENTED_EDGE ( 'NONE', *, *, #17678, .T. ) ;
#6005=CARTESIAN_POINT ( 'NONE',  ( 0.1236067977499789861, 0.3428571428571428048, -0.3804226065180614236 ) ) ;
#6012=CARTESIAN_POINT ( 'NONE',  ( -0.4749999999999999778, 3.575000000000000622, -0.09499999999999995948 ) ) ;
#6015=CARTESIAN_POINT ( 'NONE',  ( 0.1116596296178199027, 0.05089285704531473081, 0.3436530038418508792 ) ) ;
#6018=CARTESIAN_POINT ( 'NONE',  ( 0.2233192592356399164, 0.3580357141881718164, 0.3073725909049500604 ) ) ;
#6029=EDGE_CURVE ( 'NONE', #22719, #16231, #22148, .T. ) ;
#6035=ORIENTED_EDGE ( 'NONE', *, *, #14007, .F. ) ;
#6036=ORIENTED_EDGE ( 'NONE', *, *, #4978, .F. ) ;
#6056=CARTESIAN_POINT ( 'NONE',  ( -0.3949525857693607089, 5.436648244187127775E-19, 0.06334394204733222178 ) ) ;
#6064=DIRECTION ( 'NONE',  ( 0.000000000000000000, 0.000000000000000000, -1.000000000000000000 ) ) ;
#6074=CARTESIAN_POINT ( 'NONE',  ( 2.326421213736078119E-17, -0.05982142866897093708, -0.3799334167787516425 ) ) ;
#6082=CARTESIAN_POINT ( 'NONE',  ( -0.2048996585731238107, 1.937136306180702348E-16, -0.3358682071059586050 ) ) ;
#6087=CARTESIAN_POINT ( 'NONE',  ( 0.000000000000000000, 3.700000000000000622, 0.000000000000000000 ) ) ;
#6092=CARTESIAN_POINT ( 'NONE',  ( -0.1116596296178200276, 0.4008928570453146878, 0.3436530038418508792 ) ) ;
#6102=CARTESIAN_POINT ( 'NONE',  ( 0.4000000000000000222, 0.2571428571428571175, 0.000000000000000000 ) ) ;
#6105=CARTESIAN_POINT ( 'NONE',  ( -0.2472135954999579444, 0.3446428569477722470, -0.3402603233408160732 ) ) ;
#6106=CARTESIAN_POINT ( 'NONE',  ( 0.3236067977499790249, 0.1928571428571428104, -0.2351141009169892826 ) ) ;
#6114=CARTESIAN_POINT ( 'NONE',  ( 0.3236067977499790249, 0.3267857140906294533, -0.2351141009169892826 ) ) ;
#6122=CARTESIAN_POINT ( 'NONE',  ( -7.000945310522701902E-17, 0.4446428569477722803, 0.3999999999999999667 ) ) ;
#6124=VERTEX_POINT ( 'NONE', #20023 ) ;
#6130=VECTOR ( 'NONE', #16083, 39.37007874015748143 ) ;
#6131=ORIENTED_EDGE ( 'NONE', *, *, #14723, .F. ) ;
#6135=CARTESIAN_POINT ( 'NONE',  ( -0.2233192592356399997, 0.1116071427596004306, 0.3073725909049499494 ) ) ;
#6139=CARTESIAN_POINT ( 'NONE',  ( -0.2233192592356399442, 0.2508928570453147211, -0.3073725909049499494 ) ) ;
#6151=ORIENTED_EDGE ( 'NONE', *, *, #179, .F. ) ;
#6152=CARTESIAN_POINT ( 'NONE',  ( -0.1116596296178199582, 0.3008928570453147100, -0.3436530038418508792 ) ) ;
#6171=CARTESIAN_POINT ( 'NONE',  ( -0.3999999999999999667, 0.4232142855192009279, -0.1299678784931626030 ) ) ;
#6175=CARTESIAN_POINT ( 'NONE',  ( -0.06281267474701307529, 1.673690498276176774E-18, 0.3705465256992553913 ) ) ;
#6192=CARTESIAN_POINT ( 'NONE',  ( 0.1116596296178199027, 0.4258928570453147100, 0.3436530038418508792 ) ) ;
#6199=( BOUNDED_CURVE ( )  B_SPLINE_CURVE ( 2, ( #1608, #18666, #9160, #1838, #1486, #18427, #3672, #1966, #9042, #5378, #16488, #7573, #3549 ),
 .UNSPECIFIED., .F., .F. ) 
 B_SPLINE_CURVE_WITH_KNOTS ( ( 3, 2, 2, 2, 2, 2, 3 ),
 ( 0.5357142857142856984, 0.5428571428571428159, 0.5571428571428571619, 0.5714285714285713969, 0.5857142857142857428, 0.5999999999999999778, 0.6071428571428572063 ),
 .UNSPECIFIED. ) 
 CURVE ( )  GEOMETRIC_REPRESENTATION_ITEM ( )  RATIONAL_B_SPLINE_CURVE ( ( 0.9755282581475768211, 0.9755282581475768211, 1.000000000000000000, 0.9510565162951535312, 1.000000000000000000, 0.9510565162951535312, 1.000000000000000000, 0.9510565162951535312, 1.000000000000000000, 0.9510565162951535312, 1.000000000000000000, 0.9755282581475765991, 0.9755282581475768211 ) ) 
 REPRESENTATION_ITEM ( '' )  );
#6202=CARTESIAN_POINT ( 'NONE',  ( 0.1952751578279883771, -4.088425335522479322E-18, -0.3153013832115701409 ) ) ;
#6207=EDGE_CURVE ( 'NONE', #22719, #16849, #1582, .T. ) ;
#6210=DIRECTION ( 'NONE',  ( -0.000000000000000000, -1.000000000000000000, -0.000000000000000000 ) ) ;
#6215=DIRECTION ( 'NONE',  ( -0.000000000000000000, -1.000000000000000000, -0.000000000000000000 ) ) ;
#6227=CARTESIAN_POINT ( 'NONE',  ( 0.000000000000000000, 3.575000000000000622, 0.000000000000000000 ) ) ;
#6230=DIRECTION ( 'NONE',  ( 0.000000000000000000, -1.000000000000000000, 0.000000000000000000 ) ) ;
#6235=CARTESIAN_POINT ( 'NONE',  ( -7.726019084026502927E-17, 0.3732142855192007724, 0.4205848896953069405 ) ) ;
#6250=CARTESIAN_POINT ( 'NONE',  ( 0.3999999999999999667, 0.3321428571428570176, -0.1299678784931625197 ) ) ;
#6259=CARTESIAN_POINT ( 'NONE',  ( -0.3613381517857143232, 0.1687499999024575370, -0.1174058825155741004 ) ) ;
#6263=CARTESIAN_POINT ( 'NONE',  ( -0.2233192592356400275, 0.2723214284738861291, 0.3073725909049499494 ) ) ;
#6264=CARTESIAN_POINT ( 'NONE',  ( -0.1236067977499789583, 0.1267857140906294700, -0.3804226065180614791 ) ) ;
#6275=CARTESIAN_POINT ( 'NONE',  ( -0.3613381517857143232, 0.2437499999024575481, -4.425116109941954795E-17 ) ) ;
#6289=ORIENTED_EDGE ( 'NONE', *, *, #16454, .T. ) ;
#6293=ORIENTED_EDGE ( 'NONE', *, *, #20654, .F. ) ;
#6303=CARTESIAN_POINT ( 'NONE',  ( -0.3116633505738114485, 3.673292957400295933, 0.09499999999999995948 ) ) ;
#6313=ADVANCED_FACE ( 'NONE', ( #16221 ), #1461, .T. ) ;
#6314=CARTESIAN_POINT ( 'NONE',  ( 0.2923287055106771337, 0.05803571418817188299, 0.2123892367102621359 ) ) ;
#6330=ORIENTED_EDGE ( 'NONE', *, *, #23214, .T. ) ;
#6347=CARTESIAN_POINT ( 'NONE',  ( 0.3255746755405797832, 3.686631053106446565, 0.09499999999999995948 ) ) ;
#6360=CARTESIAN_POINT ( 'NONE',  ( -0.2472135954999579999, 0.3660714283763437660, 0.3402603233408159622 ) ) ;
#6371=ADVANCED_FACE ( 'NONE', ( #918 ), #12040, .T. ) ;
#6382=CARTESIAN_POINT ( 'NONE',  ( -0.1116596296178200276, 0.1866071427596004417, 0.3436530038418508792 ) ) ;
#6384=CARTESIAN_POINT ( 'NONE',  ( -0.2233192592356399442, 0.3937499999024575148, -0.3073725909049499494 ) ) ;
#6385=CARTESIAN_POINT ( 'NONE',  ( -0.3236067977499789694, 0.1339285712334866152, -0.2351141009169893104 ) ) ;
#6388=CARTESIAN_POINT ( 'NONE',  ( 0.000000000000000000, 0.02999999999999995379, -0.3125000000000000000 ) ) ;
#6396=CARTESIAN_POINT ( 'NONE',  ( 0.3613381517857143232, 0.2794642856167433020, 0.000000000000000000 ) ) ;
#6397=ORIENTED_EDGE ( 'NONE', *, *, #23603, .T. ) ;
#6433=CARTESIAN_POINT ( 'NONE',  ( -0.2923287055106771337, -0.03482142866897096345, 0.2123892367102619971 ) ) ;
#6436=DIRECTION ( 'NONE',  ( 0.000000000000000000, 1.000000000000000000, 0.000000000000000000 ) ) ;
#6450=CARTESIAN_POINT ( 'NONE',  ( 0.3614195271177944591, -9.204707668395282654E-18, -0.008981461429929990525 ) ) ;
#6456=CARTESIAN_POINT ( 'NONE',  ( -0.3613381517857143788, 0.3901785713310290116, 0.1174058825155740310 ) ) ;
#6463=FACE_OUTER_BOUND ( 'NONE', #4802, .T. ) ;
#6469=CARTESIAN_POINT ( 'NONE',  ( 0.3236067977499789694, 0.3928571428571427382, 0.2351141009169893659 ) ) ;
#6477=EDGE_CURVE ( 'NONE', #769, #16532, #12421, .T. ) ;
#6479=CARTESIAN_POINT ( 'NONE',  ( -0.1236067977499790416, 0.3696428569477723247, 0.3804226065180614236 ) ) ;
#6503=CARTESIAN_POINT ( 'NONE',  ( 2.326421213736078119E-17, 0.3687499999024574371, -0.3799334167787516425 ) ) ;
#6504=DIRECTION ( 'NONE',  ( -0.000000000000000000, -1.000000000000000000, -0.000000000000000000 ) ) ;
#6506=CIRCLE ( 'NONE', #17408, 0.7199999999999994182 ) ;
#6535=CYLINDRICAL_SURFACE ( 'NONE', #14137, 0.4000000000000000222 ) ;
#6550=CARTESIAN_POINT ( 'NONE',  ( -0.3613381517857144343, 0.2473214284738860791, 0.1174058825155740171 ) ) ;
#6559=CARTESIAN_POINT ( 'NONE',  ( 0.1236067977499789028, 0.09999999999999997780, 0.3804226065180614791 ) ) ;
#6574=CARTESIAN_POINT ( 'NONE',  ( 0.2233192592356400275, 0.004464285616743319737, -0.3073725909049499494 ) ) ;
#6585=CARTESIAN_POINT ( 'NONE',  ( 0.2233192592356399164, 0.0008928570453147456013, 0.3073725909049500604 ) ) ;
#6598=CARTESIAN_POINT ( 'NONE',  ( 0.1116596296178199027, -0.002678571526113819427, 0.3436530038418508792 ) ) ;
#6613=EDGE_LOOP ( 'NONE', ( #8129, #10426, #16240, #10292 ) ) ;
#6618=CARTESIAN_POINT ( 'NONE',  ( -0.1116596296178199582, 0.2294642856167432854, -0.3436530038418508792 ) ) ;
#6635=ORIENTED_EDGE ( 'NONE', *, *, #935, .T. ) ;
#6645=DIRECTION ( 'NONE',  ( -0.000000000000000000, 1.000000000000000000, -0.000000000000000000 ) ) ;
#6669=CARTESIAN_POINT ( 'NONE',  ( -0.2923287055106771337, 0.3973214284738861291, -0.2123892367102620804 ) ) ;
#6671=PLANE ( 'NONE',  #22017 ) ;
#6673=CARTESIAN_POINT ( 'NONE',  ( -0.2233192592356399997, 0.1830357141881718830, 0.3073725909049499494 ) ) ;
#6687=CARTESIAN_POINT ( 'NONE',  ( 9.101228903679513089E-16, 0.2392857142857141850, 0.4000000000000000222 ) ) ;
#6703=CARTESIAN_POINT ( 'NONE',  ( -0.2923287055106771337, 0.04017857133102902684, -0.2123892367102620804 ) ) ;
#6717=CARTESIAN_POINT ( 'NONE',  ( -0.2233192592356399442, -0.03482142866897095651, -0.3073725909049500049 ) ) ;
#6733=AXIS2_PLACEMENT_3D ( 'NONE', #3939, #18809, #2105 ) ;
#6740=CARTESIAN_POINT ( 'NONE',  ( -0.2233192592356399997, 0.2544642856167432243, 0.3073725909049499494 ) ) ;
#6751=CARTESIAN_POINT ( 'NONE',  ( -0.4749999999999999778, 3.575000000000000622, 0.09499999999999995948 ) ) ;
#6759=ORIENTED_EDGE ( 'NONE', *, *, #13343, .T. ) ;
#6793=CARTESIAN_POINT ( 'NONE',  ( -0.3613381517857143232, 0.4008928570453146878, -0.1174058825155741004 ) ) ;
#6797=( BOUNDED_CURVE ( )  B_SPLINE_CURVE ( 2, ( #14847, #17677, #964, #6574, #21567, #14024, #8521, #15961, #4860, #12326, #19085, #16786, #16897, #9830, #432, #1902, #17017, #5915, #13144, #13262, #9584, #2270, #5681, #14959, #17264, #7865, #9343, #312, #13375, #20559, #20679, #7749, #9705, #2148, #15314, #15193, #22744, #3970, #20438, #15081, #7982, #13500, #20915, #7630, #20796, #18850, #4209, #7512, #2393, #22262, #11661, #11542, #11181, #22631, #18610, #189, #22502, #547, #67, #5799, #22378, #11419, #11297, #5558, #13023, #3734, #18729, #2025, #672, #22972, #6275, #10073, #17494, #13731, #4442, #9949, #8218, #23088, #21278, #12030, #6396, #13847, #19442, #13617, #15435, #22861, #6152, #21032, #4325, #11778, #20972, #8280, #19385, #15372, #23032, #731, #15730, #23144, #9765, #19142, #2450, #13679, #5970, #611, #8042, #18911, #7810, #9889, #17436, #4147, #17317, #6456, #13908, #15491, #6092, #17203, #22920, #22800, #9642, #2211, #4269 ),
 .UNSPECIFIED., .F., .F. ) 
 B_SPLINE_CURVE_WITH_KNOTS ( ( 3, 2, 2, 2, 2, 2, 2, 2, 2, 2, 2, 2, 2, 2, 2, 2, 2, 2, 2, 2, 2, 2, 2, 2, 2, 2, 2, 2, 2, 2, 2, 2, 2, 2, 2, 2, 2, 2, 2, 2, 2, 2, 2, 2, 2, 2, 2, 2, 2, 2, 2, 2, 2, 2, 2, 2, 2, 2, 2, 2, 3 ),
 ( 0.1552981728545431983, 0.1571428571428571397, 0.1714285714285714302, 0.1857142857142857206, 0.2000000000000000111, 0.2142857142857142738, 0.2285714285714285643, 0.2428571428571428548, 0.2571428571428571175, 0.2714285714285714080, 0.2857142857142856984, 0.2999999999999999889, 0.3142857142857142794, 0.3285714285714285698, 0.3428571428571428603, 0.3571428571428571508, 0.3714285714285714413, 0.3857142857142857872, 0.4000000000000000222, 0.4142857142857142572, 0.4285714285714284921, 0.4428571428571428381, 0.4571428571428570731, 0.4714285714285714191, 0.4857142857142856540, 0.5000000000000000000, 0.5142857142857143460, 0.5285714285714285809, 0.5428571428571428159, 0.5571428571428571619, 0.5714285714285713969, 0.5857142857142857428, 0.5999999999999999778, 0.6142857142857144348, 0.6285714285714285587, 0.6428571428571429047, 0.6571428571428571397, 0.6714285714285713746, 0.6857142857142857206, 0.6999999999999999556, 0.7142857142857143016, 0.7285714285714285365, 0.7428571428571428825, 0.7571428571428572285, 0.7714285714285714635, 0.7857142857142856984, 0.8000000000000000444, 0.8142857142857142794, 0.8285714285714286254, 0.8428571428571428603, 0.8571428571428570953, 0.8714285714285713302, 0.8857142857142855652, 0.9000000000000000222, 0.9142857142857142572, 0.9285714285714286031, 0.9428571428571428381, 0.9571428571428571841, 0.9714285714285714191, 0.9857142857142857650, 1.000000000000000000 ),
 .UNSPECIFIED. ) 
 CURVE ( )  GEOMETRIC_REPRESENTATION_ITEM ( )  RATIONAL_B_SPLINE_CURVE ( ( 0.9889922301674729521, 0.9936800307216023809, 1.000000000000000000, 0.9510565162951535312, 1.000000000000000000, 0.9510565162951535312, 1.000000000000000000, 0.9510565162951535312, 1.000000000000000000, 0.9510565162951535312, 1.000000000000000000, 0.9510565162951535312, 1.000000000000000000, 0.9510565162951535312, 1.000000000000000000, 0.9510565162951535312, 1.000000000000000000, 0.9510565162951535312, 1.000000000000000000, 0.9510565162951535312, 1.000000000000000000, 0.9510565162951535312, 1.000000000000000000, 0.9510565162951535312, 1.000000000000000000, 0.9510565162951535312, 1.000000000000000000, 0.9510565162951535312, 1.000000000000000000, 0.9510565162951535312, 1.000000000000000000, 0.9510565162951535312, 1.000000000000000000, 0.9510565162951535312, 1.000000000000000000, 0.9510565162951535312, 1.000000000000000000, 0.9510565162951535312, 1.000000000000000000, 0.9510565162951535312, 1.000000000000000000, 0.9510565162951535312, 1.000000000000000000, 0.9510565162951535312, 1.000000000000000000, 0.9510565162951535312, 1.000000000000000000, 0.9510565162951535312, 1.000000000000000000, 0.9510565162951535312, 1.000000000000000000, 0.9510565162951535312, 1.000000000000000000, 0.9510565162951535312, 1.000000000000000000, 0.9510565162951535312, 1.000000000000000000, 0.9510565162951535312, 1.000000000000000000, 0.9510565162951535312, 1.000000000000000000, 0.9510565162951535312, 1.000000000000000000, 0.9510565162951535312, 1.000000000000000000, 0.9510565162951535312, 1.000000000000000000, 0.9510565162951535312, 1.000000000000000000, 0.9510565162951535312, 1.000000000000000000, 0.9510565162951535312, 1.000000000000000000, 0.9510565162951535312, 1.000000000000000000, 0.9510565162951535312, 1.000000000000000000, 0.9510565162951535312, 1.000000000000000000, 0.9510565162951535312, 1.000000000000000000, 0.9510565162951535312, 1.000000000000000000, 0.9510565162951535312, 1.000000000000000000, 0.9510565162951535312, 1.000000000000000000, 0.9510565162951535312, 1.000000000000000000, 0.9510565162951535312, 1.000000000000000000, 0.9510565162951535312, 1.000000000000000000, 0.9510565162951535312, 1.000000000000000000, 0.9510565162951535312, 1.000000000000000000, 0.9510565162951535312, 1.000000000000000000, 0.9510565162951535312, 1.000000000000000000, 0.9510565162951535312, 1.000000000000000000, 0.9510565162951535312, 1.000000000000000000, 0.9510565162951535312, 1.000000000000000000, 0.9510565162951535312, 1.000000000000000000, 0.9510565162951535312, 1.000000000000000000, 0.9510565162951535312, 1.000000000000000000, 0.9510565162951535312, 1.000000000000000000, 0.9510565162951535312, 1.000000000000000000, 0.9510565162951535312, 1.000000000000000000, 0.9510565162951535312, 1.000000000000000000 ) ) 
 REPRESENTATION_ITEM ( '' )  );
#6798=CARTESIAN_POINT ( 'NONE',  ( 0.1116596296178199027, 0.2651785713310289561, 0.3436530038418508792 ) ) ;
#6802=DIRECTION ( 'NONE',  ( 0.000000000000000000, 0.000000000000000000, 1.000000000000000000 ) ) ;
#6811=CARTESIAN_POINT ( 'NONE',  ( 0.000000000000000000, -2.347681869555226049E-17, 0.3425000000000000266 ) ) ;
#6814=DIRECTION ( 'NONE',  ( 1.000000000000000000, -0.000000000000000000, 1.224646799147353207E-16 ) ) ;
#6816=EDGE_CURVE ( 'NONE', #17359, #15714, #19429, .T. ) ;
#6828=CARTESIAN_POINT ( 'NONE',  ( -0.3613381517857143232, 0.04374999990245759252, -0.1174058825155741004 ) ) ;
#6841=CARTESIAN_POINT ( 'NONE',  ( -0.3613381517857143232, -0.02767857152611381474, -0.1174058825155741004 ) ) ;
#6859=VERTEX_POINT ( 'NONE', #9815 ) ;
#6862=CARTESIAN_POINT ( 'NONE',  ( 0.4749999999999999778, 3.700000000000000622, -0.09499999999999995948 ) ) ;
#6864=CARTESIAN_POINT ( 'NONE',  ( -0.3236067977499790249, 0.08571428571428568732, 0.2351141009169892271 ) ) ;
#6867=CYLINDRICAL_SURFACE ( 'NONE', #7689, 0.7500000000000001110 ) ;
#6887=ADVANCED_FACE ( 'NONE', ( #17968 ), #8934, .T. ) ;
#6904=DIRECTION ( 'NONE',  ( -0.000000000000000000, -1.000000000000000000, -0.000000000000000000 ) ) ;
#6915=CARTESIAN_POINT ( 'NONE',  ( 0.3613381517857143232, 0.3651785713310288783, 0.1174058825155742114 ) ) ;
#6919=CARTESIAN_POINT ( 'NONE',  ( -0.1116596296178200276, 0.1866071427596004417, 0.3436530038418508792 ) ) ;
#6925=EDGE_CURVE ( 'NONE', #20833, #7372, #20393, .T. ) ;
#6936=ORIENTED_EDGE ( 'NONE', *, *, #6029, .F. ) ;
#6952=CARTESIAN_POINT ( 'NONE',  ( -0.3613381517857144343, 0.05089285704531474469, 0.1174058825155740171 ) ) ;
#6958=EDGE_CURVE ( 'NONE', #17046, #18346, #1907, .T. ) ;
#6961=CARTESIAN_POINT ( 'NONE',  ( -0.4000000000000000222, 0.07857142857142855596, -4.898587196589413075E-17 ) ) ;
#6965=AXIS2_PLACEMENT_3D ( 'NONE', #17272, #4335, #13741 ) ;
#6966=CARTESIAN_POINT ( 'NONE',  ( 0.2923287055106771337, 0.07589285704531474608, 0.2123892367102621359 ) ) ;
#6974=CARTESIAN_POINT ( 'NONE',  ( 0.000000000000000000, 3.659999999999999698, -0.3125000000000000000 ) ) ;
#6978=VERTEX_POINT ( 'NONE', #13771 ) ;
#6985=EDGE_CURVE ( 'NONE', #22531, #4780, #2319, .T. ) ;
#6988=CARTESIAN_POINT ( 'NONE',  ( 0.3236067977499789694, -0.03571428571428573312, 0.2351141009169893659 ) ) ;
#7000=VECTOR ( 'NONE', #22409, 39.37007874015748143 ) ;
#7011=AXIS2_PLACEMENT_3D ( 'NONE', #16525, #16646, #46 ) ;
#7041=CARTESIAN_POINT ( 'NONE',  ( -0.2923287055106771337, 0.3401785713310290227, 0.2123892367102619971 ) ) ;
#7043=CARTESIAN_POINT ( 'NONE',  ( 0.3236067977499790249, 0.04999999999999996114, -0.2351141009169892826 ) ) ;
#7045=CARTESIAN_POINT ( 'NONE',  ( -0.3613381517857143232, 0.1723214284738861513, -4.425116109941954795E-17 ) ) ;
#7063=EDGE_CURVE ( 'NONE', #7566, #5247, #1556, .T. ) ;
#7075=CARTESIAN_POINT ( 'NONE',  ( -0.3613381517857143232, 0.1151785713310290032, -0.1174058825155741004 ) ) ;
#7082=ORIENTED_EDGE ( 'NONE', *, *, #6985, .T. ) ;
#7083=CARTESIAN_POINT ( 'NONE',  ( -0.06335377612981435425, 0.09459806137332689435, 0.4000000000000000777 ) ) ;
#7087=CARTESIAN_POINT ( 'NONE',  ( -0.3613381517857144343, 0.05089285704531475163, 0.1174058825155740171 ) ) ;
#7095=CARTESIAN_POINT ( 'NONE',  ( 0.1236067977499789028, 0.3857142857142856207, 0.3804226065180614791 ) ) ;
#7098=EDGE_CURVE ( 'NONE', #16665, #20411, #9126, .T. ) ;
#7099=CARTESIAN_POINT ( 'NONE',  ( 0.2472135954999579166, 0.2374999998049151795, 0.3402603233408160732 ) ) ;
#7108=CARTESIAN_POINT ( 'NONE',  ( 0.000000000000000000, 3.700000000000000622, -0.7199999999999994182 ) ) ;
#7110=CARTESIAN_POINT ( 'NONE',  ( -0.2472135954999579999, 0.01785714285714282493, 0.3402603233408159622 ) ) ;
#7161=CARTESIAN_POINT ( 'NONE',  ( 0.3613381517857143232, 0.3687499999024574926, 0.000000000000000000 ) ) ;
#7162=CARTESIAN_POINT ( 'NONE',  ( 0.06335377612981431261, 0.05888377565904120980, -0.4000000000000000777 ) ) ;
#7163=CARTESIAN_POINT ( 'NONE',  ( 0.2233192592356399164, 0.4116071427596004750, 0.3073725909049500604 ) ) ;
#7177=AXIS2_PLACEMENT_3D ( 'NONE', #8311, #10284, #17707 ) ;
#7192=CARTESIAN_POINT ( 'NONE',  ( -0.3613381517857143232, 0.3294642856167431799, -0.1174058825155741004 ) ) ;
#7204=CARTESIAN_POINT ( 'NONE',  ( -0.1116596296178200276, 0.1330357141881718663, 0.3436530038418508792 ) ) ;
#7208=CYLINDRICAL_SURFACE ( 'NONE', #15887, 0.09499999999999995948 ) ;
#7222=CARTESIAN_POINT ( 'NONE',  ( 0.4749999999999999778, 3.700000000000000622, 2.908536147974959276E-17 ) ) ;
#7231=CARTESIAN_POINT ( 'NONE',  ( -0.4000000000000000222, -0.06428571428571429325, -4.898587196589413075E-17 ) ) ;
#7233=DIRECTION ( 'NONE',  ( 0.000000000000000000, 0.000000000000000000, 1.000000000000000000 ) ) ;
#7237=CARTESIAN_POINT ( 'NONE',  ( 2.575339694675500462E-17, 0.1946428569477723081, -0.4205848896953069405 ) ) ;
#7239=EDGE_CURVE ( 'NONE', #22475, #8827, #4700, .T. ) ;
#7249=VECTOR ( 'NONE', #22566, 39.37007874015748143 ) ;
#7259=CARTESIAN_POINT ( 'NONE',  ( 0.3613381517857143232, 0.4312499999024575481, 0.000000000000000000 ) ) ;
#7261=CARTESIAN_POINT ( 'NONE',  ( 1.750236327630675537E-16, 0.08749999980491518503, 0.3999999999999999667 ) ) ;
#7264=CARTESIAN_POINT ( 'NONE',  ( -0.1116596296178200276, 0.2044642856167432909, 0.3436530038418508792 ) ) ;
#7276=ORIENTED_EDGE ( 'NONE', *, *, #13343, .F. ) ;
#7284=CARTESIAN_POINT ( 'NONE',  ( 0.2923287055106771337, 0.3580357141881718164, -0.2123892367102620249 ) ) ;
#7287=ADVANCED_FACE ( 'NONE', ( #23103 ), #13865, .T. ) ;
#7295=CARTESIAN_POINT ( 'NONE',  ( 0.1633221850526035690, 2.539511724522410611E-17, 0.3257820047251743789 ) ) ;
#7313=CARTESIAN_POINT ( 'NONE',  ( 0.2923287055106771337, 0.2187499999024575537, 0.2123892367102621359 ) ) ;
#7319=ORIENTED_EDGE ( 'NONE', *, *, #6958, .F. ) ;
#7325=CARTESIAN_POINT ( 'NONE',  ( -0.3613381517857143232, 0.1901785713310290282, -4.425116109941954795E-17 ) ) ;
#7334=DIRECTION ( 'NONE',  ( -0.000000000000000000, -1.000000000000000000, -0.000000000000000000 ) ) ;
#7346=CARTESIAN_POINT ( 'NONE',  ( -0.1236067977499789583, 0.06428571428571425161, -0.3804226065180614791 ) ) ;
#7353=CARTESIAN_POINT ( 'NONE',  ( 0.3236067977499790249, 0.1839285712334866596, -0.2351141009169892826 ) ) ;
#7372=VERTEX_POINT ( 'NONE', #21980 ) ;
#7374=DIRECTION ( 'NONE',  ( -0.000000000000000000, 1.000000000000000000, -0.000000000000000000 ) ) ;
#7379=CARTESIAN_POINT ( 'NONE',  ( 0.2923287055106771337, 0.07589285704531474608, 0.2123892367102621359 ) ) ;
#7392=ADVANCED_FACE ( 'NONE', ( #23796, #5153 ), #12618, .T. ) ;
#7403=ORIENTED_EDGE ( 'NONE', *, *, #22883, .T. ) ;
#7405=CARTESIAN_POINT ( 'NONE',  ( -0.3613381517857143232, 0.3830357141881717276, -0.1174058825155741004 ) ) ;
#7412=CIRCLE ( 'NONE', #9362, 0.3125000000000000000 ) ;
#7427=ADVANCED_FACE ( 'NONE', ( #12744 ), #13838, .T. ) ;
#7433=CARTESIAN_POINT ( 'NONE',  ( -0.2923287055106771337, 0.1830357141881718552, -0.2123892367102620804 ) ) ;
#7443=CARTESIAN_POINT ( 'NONE',  ( -0.1116596296178200276, 0.2044642856167432909, 0.3436530038418508792 ) ) ;
#7457=ORIENTED_EDGE ( 'NONE', *, *, #5933, .T. ) ;
#7460=DIRECTION ( 'NONE',  ( 0.000000000000000000, 0.000000000000000000, 1.000000000000000000 ) ) ;
#7462=CARTESIAN_POINT ( 'NONE',  ( 0.1236067977499789861, 0.2714285714285713524, -0.3804226065180614236 ) ) ;
#7470=CARTESIAN_POINT ( 'NONE',  ( 0.1236067977499789028, 0.01964285694777236080, 0.3804226065180614791 ) ) ;
#7471=CARTESIAN_POINT ( 'NONE',  ( -0.2815565333327582631, -9.420544349976224069E-18, -0.2815901784494979077 ) ) ;
#7489=ORIENTED_EDGE ( 'NONE', *, *, #11572, .T. ) ;
#7494=CARTESIAN_POINT ( 'NONE',  ( 2.326421213736078119E-17, 0.1544642856167433020, -0.3799334167787516425 ) ) ;
#7498=CARTESIAN_POINT ( 'NONE',  ( -0.2233192592356399442, 0.1794642856167432687, -0.3073725909049499494 ) ) ;
#7512=CARTESIAN_POINT ( 'NONE',  ( -0.2233192592356399442, 0.1616071427596004473, -0.3073725909049499494 ) ) ;
#7515=CARTESIAN_POINT ( 'NONE',  ( 9.101228903679513089E-16, 0.3732142855192008835, 0.4000000000000000222 ) ) ;
#7522=EDGE_CURVE ( 'NONE', #3235, #20411, #22044, .T. ) ;
#7539=VERTEX_POINT ( 'NONE', #19978 ) ;
#7547=CARTESIAN_POINT ( 'NONE',  ( 0.1116596296178199860, 0.3830357141881718386, -0.3436530038418508792 ) ) ;
#7559=CARTESIAN_POINT ( 'NONE',  ( 0.2923287055106771337, 0.1473214284738861568, 0.2123892367102621359 ) ) ;
#7564=CARTESIAN_POINT ( 'NONE',  ( 0.3600616651536501234, -9.204707668395288817E-18, -0.03256283952987127500 ) ) ;
#7566=VERTEX_POINT ( 'NONE', #20341 ) ;
#7572=CARTESIAN_POINT ( 'NONE',  ( 0.000000000000000000, 3.659999999999999698, 0.000000000000000000 ) ) ;
#7573=CARTESIAN_POINT ( 'NONE',  ( 0.06335377612981404893, 0.2017409185161840035, -0.4000000000000001887 ) ) ;
#7583=CARTESIAN_POINT ( 'NONE',  ( 2.575339694675500462E-17, 0.1321428571428571175, -0.4205848896953069405 ) ) ;
#7584=DIRECTION ( 'NONE',  ( -0.000000000000000000, -1.000000000000000000, -0.000000000000000000 ) ) ;
#7590=CARTESIAN_POINT ( 'NONE',  ( 2.575339694675500462E-17, -0.01964285733794191718, -0.4205848896953069405 ) ) ;
#7610=LINE ( 'NONE', #7259, #3945 ) ;
#7612=CARTESIAN_POINT ( 'NONE',  ( -0.1116596296178199582, 0.1580357141881718608, -0.3436530038418508792 ) ) ;
#7616=CARTESIAN_POINT ( 'NONE',  ( -0.3613381517857143232, 0.1151785713310289894, -0.1174058825155741143 ) ) ;
#7617=ORIENTED_EDGE ( 'NONE', *, *, #14815, .F. ) ;
#7625=AXIS2_PLACEMENT_3D ( 'NONE', #23401, #12224, #19634 ) ;
#7630=CARTESIAN_POINT ( 'NONE',  ( 0.2233192592356400275, 0.1473214284738861568, -0.3073725909049499494 ) ) ;
#7643=CARTESIAN_POINT ( 'NONE',  ( 0.2233192592356399164, 0.3401785713310290227, 0.3073725909049500604 ) ) ;
#7668=CARTESIAN_POINT ( 'NONE',  ( -0.1116596296178200276, 0.2758928570453147433, 0.3436530038418508792 ) ) ;
#7680=DIRECTION ( 'NONE',  ( 0.000000000000000000, 0.000000000000000000, -1.000000000000000000 ) ) ;
#7689=AXIS2_PLACEMENT_3D ( 'NONE', #14435, #23313, #16385 ) ;
#7703=CARTESIAN_POINT ( 'NONE',  ( -7.726019084026502927E-17, 0.09642857142857139130, 0.4205848896953069405 ) ) ;
#7711=CARTESIAN_POINT ( 'NONE',  ( 0.3236067977499789694, 0.1696428569477723136, 0.2351141009169893659 ) ) ;
#7726=ORIENTED_EDGE ( 'NONE', *, *, #21482, .F. ) ;
#7729=CYLINDRICAL_SURFACE ( 'NONE', #7011, 0.3125000000000000000 ) ;
#7732=CARTESIAN_POINT ( 'NONE',  ( -0.2233192592356399997, -0.03125000009754239083, 0.3073725909049499494 ) ) ;
#7735=CARTESIAN_POINT ( 'NONE',  ( 0.1116596296178199027, 0.1401785713310290393, 0.3436530038418508792 ) ) ;
#7749=CARTESIAN_POINT ( 'NONE',  ( -0.3613381517857143788, 0.1044642856167432993, 0.1174058825155740310 ) ) ;
#7752=ORIENTED_EDGE ( 'NONE', *, *, #9178, .T. ) ;
#7758=AXIS2_PLACEMENT_3D ( 'NONE', #14438, #2757, #22990 ) ;
#7771=CARTESIAN_POINT ( 'NONE',  ( -0.2956994556028983423, 7.507838726391301300E-19, 0.2548636319900752789 ) ) ;
#7789=CARTESIAN_POINT ( 'NONE',  ( 0.2233192592356399997, 0.07589285704531473220, -0.3073725909049500049 ) ) ;
#7797=CARTESIAN_POINT ( 'NONE',  ( 0.3236067977499790249, 0.1124999998049151795, -0.2351141009169892826 ) ) ;
#7807=CARTESIAN_POINT ( 'NONE',  ( 0.3999999999999999667, 0.3160714283763437216, 0.1299678784931626307 ) ) ;
#7810=CARTESIAN_POINT ( 'NONE',  ( -0.1116596296178199582, 0.3723214284738861068, -0.3436530038418508792 ) ) ;
#7819=CARTESIAN_POINT ( 'NONE',  ( 0.1236067977499789861, 0.2714285714285713524, -0.3804226065180614236 ) ) ;
#7822=CARTESIAN_POINT ( 'NONE',  ( 0.3236067977499789694, 0.1785714285714284921, 0.2351141009169893659 ) ) ;
#7830=CARTESIAN_POINT ( 'NONE',  ( -0.3236067977499789694, 0.4196428569477723136, -0.2351141009169893104 ) ) ;
#7843=ORIENTED_EDGE ( 'NONE', *, *, #14237, .T. ) ;
#7849=CARTESIAN_POINT ( 'NONE',  ( 0.2923287055106771337, 0.1294642856167433076, 0.2123892367102621359 ) ) ;
#7851=ORIENTED_EDGE ( 'NONE', *, *, #16115, .T. ) ;
#7852=CARTESIAN_POINT ( 'NONE',  ( 2.326421213736078119E-17, 0.3866071427596002863, -0.3799334167787516980 ) ) ;
#7859=CARTESIAN_POINT ( 'NONE',  ( 0.4749999999999999778, 3.575000000000000622, -0.09499999999999995948 ) ) ;
#7865=CARTESIAN_POINT ( 'NONE',  ( 2.326421213736078119E-17, 0.08303571418817184968, -0.3799334167787516980 ) ) ;
#7887=CARTESIAN_POINT ( 'NONE',  ( 1.750236327630675475E-17, 0.2749999999999999112, -0.3999999999999999667 ) ) ;
#7899=CARTESIAN_POINT ( 'NONE',  ( 0.2923287055106771337, -0.01339285724039953988, 0.2123892367102621359 ) ) ;
#7905=( BOUNDED_CURVE ( )  B_SPLINE_CURVE ( 2, ( #2488, #282, #17355, #21007, #15646, #8196, #9806 ),
 .UNSPECIFIED., .F., .T. ) 
 B_SPLINE_CURVE_WITH_KNOTS ( ( 3, 2, 2, 3 ),
 ( 0.9642857142857143016, 0.9714285714285714191, 0.9857142857142857650, 1.000000000000000000 ),
 .UNSPECIFIED. ) 
 CURVE ( )  GEOMETRIC_REPRESENTATION_ITEM ( )  RATIONAL_B_SPLINE_CURVE ( ( 0.9755282581475768211, 0.9755282581475768211, 1.000000000000000000, 0.9510565162951535312, 1.000000000000000000, 0.9510565162951535312, 1.000000000000000000 ) ) 
 REPRESENTATION_ITEM ( '' )  );
#7907=CARTESIAN_POINT ( 'NONE',  ( 0.000000000000000000, 3.700000000000000622, 0.000000000000000000 ) ) ;
#7934=CARTESIAN_POINT ( 'NONE',  ( -0.1236067977499789583, 0.1357142857142856485, -0.3804226065180614791 ) ) ;
#7941=CARTESIAN_POINT ( 'NONE',  ( 2.575339694675500462E-17, 0.3374999998049151850, -0.4205848896953069405 ) ) ;
#7950=CARTESIAN_POINT ( 'NONE',  ( -0.3999999999999999667, 0.2803571426620579676, -0.1299678784931626030 ) ) ;
#7955=( GEOMETRIC_REPRESENTATION_CONTEXT ( 3 ) GLOBAL_UNCERTAINTY_ASSIGNED_CONTEXT ( ( #23356 ) ) GLOBAL_UNIT_ASSIGNED_CONTEXT ( ( #17469, #19295, #1002 ) ) REPRESENTATION_CONTEXT ( 'NONE', 'WORKASPACE' ) );
#7956=EDGE_CURVE ( 'NONE', #18530, #19679, #4773, .T. ) ;
#7963=CARTESIAN_POINT ( 'NONE',  ( -0.3999999999999999667, 0.003571428571428547898, -0.1299678784931626030 ) ) ;
#7967=CARTESIAN_POINT ( 'NONE',  ( -6.979263641208234666E-17, 0.04732142847388615819, 0.3799334167787516425 ) ) ;
#7971=CARTESIAN_POINT ( 'NONE',  ( -0.3613381517857143232, 0.3294642856167431799, -0.1174058825155741143 ) ) ;
#7982=CARTESIAN_POINT ( 'NONE',  ( 0.3613381517857143232, 0.1366071427596004251, 0.000000000000000000 ) ) ;
#7985=EDGE_CURVE ( 'NONE', #10268, #21333, #18091, .T. ) ;
#8005=LINE ( 'NONE', #4346, #10224 ) ;
#8009=PRODUCT_DEFINITION_FORMATION_WITH_SPECIFIED_SOURCE ( 'ANY', '', #3495, .NOT_KNOWN. ) ;
#8021=CARTESIAN_POINT ( 'NONE',  ( 0.2233192592356399997, -0.06696428581182808926, -0.3073725909049500049 ) ) ;
#8024=CARTESIAN_POINT ( 'NONE',  ( 0.3236067977499790249, 0.04107142837634377569, -0.2351141009169892826 ) ) ;
#8029=CARTESIAN_POINT ( 'NONE',  ( 0.1236067977499789861, 0.1196428569477723386, -0.3804226065180614236 ) ) ;
#8030=CARTESIAN_POINT ( 'NONE',  ( 0.2934658712818546955, -2.697513918649167310E-18, -0.2160150187107265918 ) ) ;
#8039=ORIENTED_EDGE ( 'NONE', *, *, #18738, .F. ) ;
#8042=CARTESIAN_POINT ( 'NONE',  ( 0.1116596296178199860, 0.3651785713310289894, -0.3436530038418508792 ) ) ;
#8057=CARTESIAN_POINT ( 'NONE',  ( -0.3999999999999999667, 0.1464285714285713802, -0.1299678784931626030 ) ) ;
#8058=CARTESIAN_POINT ( 'NONE',  ( -0.2472135954999579444, 0.3535714285714284810, -0.3402603233408159622 ) ) ;
#8065=CARTESIAN_POINT ( 'NONE',  ( -0.1236067977499789583, 0.3410714283763437993, -0.3804226065180614791 ) ) ;
#8068=CIRCLE ( 'NONE', #3793, 0.3125000000000000000 ) ;
#8071=( LENGTH_UNIT ( ) NAMED_UNIT ( * ) SI_UNIT ( $, .METRE. ) );
#8073=MECHANICAL_CONTEXT ( 'NONE', #1723, 'mechanical' ) ;
#8083=CARTESIAN_POINT ( 'NONE',  ( -0.2923287055106771337, 0.3223214284738861735, 0.2123892367102619971 ) ) ;
#8086=CARTESIAN_POINT ( 'NONE',  ( -0.1116596296178199582, 0.3187499999024575592, -0.3436530038418508792 ) ) ;
#8118=EDGE_CURVE ( 'NONE', #4381, #22719, #20587, .T. ) ;
#8129=ORIENTED_EDGE ( 'NONE', *, *, #14863, .T. ) ;
#8135=ADVANCED_FACE ( 'NONE', ( #11382 ), #22708, .F. ) ;
#8138=CARTESIAN_POINT ( 'NONE',  ( 0.2233192592356399164, 0.05446428561674330343, 0.3073725909049500604 ) ) ;
#8147=CARTESIAN_POINT ( 'NONE',  ( 0.1690789815138871444, -4.088425335522419233E-18, -0.3319522695443154481 ) ) ;
#8172=CARTESIAN_POINT ( 'NONE',  ( -4.638126268221291196E-16, 0.1321428571428571175, -0.4000000000000000222 ) ) ;
#8173=CARTESIAN_POINT ( 'NONE',  ( 0.3999999999999999667, 0.3321428571428570731, -0.1299678784931625475 ) ) ;
#8180=CARTESIAN_POINT ( 'NONE',  ( 0.3236067977499790249, 0.2553571426620580009, -0.2351141009169892826 ) ) ;
#8185=ORIENTED_EDGE ( 'NONE', *, *, #20654, .T. ) ;
#8196=CARTESIAN_POINT ( 'NONE',  ( 0.3999999999999999667, 0.4589285712334865708, 0.1299678784931626307 ) ) ;
#8205=CARTESIAN_POINT ( 'NONE',  ( 0.1116596296178199860, 0.2223214284738861402, -0.3436530038418508792 ) ) ;
#8218=CARTESIAN_POINT ( 'NONE',  ( 0.1116596296178199027, 0.2651785713310289561, 0.3436530038418508792 ) ) ;
#8239=CARTESIAN_POINT ( 'NONE',  ( -0.01610145506848609243, 4.708926481085645203E-18, 0.3730084384222186467 ) ) ;
#8258=CARTESIAN_POINT ( 'NONE',  ( -0.1116596296178199582, -0.05625000009754239222, -0.3436530038418508792 ) ) ;
#8274=CARTESIAN_POINT ( 'NONE',  ( 0.3380520187481464989, 3.229549314084639149E-17, 0.1297593444830981713 ) ) ;
#8280=CARTESIAN_POINT ( 'NONE',  ( -0.3613381517857143788, 0.3187499999024575592, 0.1174058825155740310 ) ) ;
#8303=CARTESIAN_POINT ( 'NONE',  ( -0.3236067977499789694, 0.3482142855192008613, -0.2351141009169893104 ) ) ;
#8311=CARTESIAN_POINT ( 'NONE',  ( 0.000000000000000000, 0.000000000000000000, 0.000000000000000000 ) ) ;
#8312=CIRCLE ( 'NONE', #11449, 0.7500000000000001110 ) ;
#8324=CARTESIAN_POINT ( 'NONE',  ( -0.3613381517857143232, 0.2401785713310289894, -0.1174058825155741004 ) ) ;
#8327=CARTESIAN_POINT ( 'NONE',  ( -0.1116596296178200276, 0.2758928570453147433, 0.3436530038418508792 ) ) ;
#8352=ORIENTED_EDGE ( 'NONE', *, *, #17624, .F. ) ;
#8357=DIRECTION ( 'NONE',  ( 0.000000000000000000, 0.000000000000000000, -1.000000000000000000 ) ) ;
#8371=CARTESIAN_POINT ( 'NONE',  ( 2.326421213736078119E-17, 0.2258928570453146711, -0.3799334167787516425 ) ) ;
#8379=DIRECTION ( 'NONE',  ( 0.000000000000000000, 1.000000000000000000, 0.000000000000000000 ) ) ;
#8406=CARTESIAN_POINT ( 'NONE',  ( 0.2233192592356399997, 0.09374999990245758141, -0.3073725909049500049 ) ) ;
#8411=DIRECTION ( 'NONE',  ( -0.000000000000000000, -1.000000000000000000, -0.000000000000000000 ) ) ;
#8420=CARTESIAN_POINT ( 'NONE',  ( -0.1116596296178200276, -0.009821428668970958592, 0.3436530038418508792 ) ) ;
#8423=CARTESIAN_POINT ( 'NONE',  ( 0.3999999999999999667, 0.1803571426620580176, -0.1299678784931625197 ) ) ;
#8430=CARTESIAN_POINT ( 'NONE',  ( -0.3236067977499789694, -1.707404996040164512E-17, -0.2351141009169893104 ) ) ;
#8433=SHAPE_REPRESENTATION_RELATIONSHIP ( 'NONE' , 'NONE' ,  #20236, #23350 ) ;
#8434=ORIENTED_EDGE ( 'NONE', *, *, #17350, .F. ) ;
#8446=CARTESIAN_POINT ( 'NONE',  ( -6.979263641208234666E-17, 0.1901785713310290005, 0.3799334167787516425 ) ) ;
#8462=EDGE_CURVE ( 'NONE', #16532, #12608, #21450, .T. ) ;
#8480=CARTESIAN_POINT ( 'NONE',  ( 0.000000000000000000, 3.700000000000000622, 0.000000000000000000 ) ) ;
#8495=( BOUNDED_CURVE ( )  B_SPLINE_CURVE ( 2, ( #18152, #16323, #3267, #8882, #23735, #21921, #5211, #15461, #20704, #336, #9731, #17171, #20583 ),
 .UNSPECIFIED., .F., .F. ) 
 B_SPLINE_CURVE_WITH_KNOTS ( ( 3, 2, 2, 2, 2, 2, 3 ),
 ( 0.6071428571428572063, 0.6142857142857143238, 0.6285714285714285587, 0.6428571428571429047, 0.6571428571428571397, 0.6714285714285713746, 0.6785714285714286031 ),
 .UNSPECIFIED. ) 
 CURVE ( )  GEOMETRIC_REPRESENTATION_ITEM ( )  RATIONAL_B_SPLINE_CURVE ( ( 0.9755282581475768211, 0.9755282581475769321, 1.000000000000000000, 0.9510565162951535312, 1.000000000000000000, 0.9510565162951535312, 1.000000000000000000, 0.9510565162951535312, 1.000000000000000000, 0.9510565162951535312, 1.000000000000000000, 0.9755282581475765991, 0.9755282581475768211 ) ) 
 REPRESENTATION_ITEM ( '' )  );
#8498=CARTESIAN_POINT ( 'NONE',  ( 0.1116596296178199027, 0.1223214284738861762, 0.3436530038418508792 ) ) ;
#8501=FACE_OUTER_BOUND ( 'NONE', #12916, .T. ) ;
#8504=ORIENTED_EDGE ( 'NONE', *, *, #16212, .F. ) ;
#8515=CARTESIAN_POINT ( 'NONE',  ( 0.3568845019303670818, 1.003480569432281344E-17, 0.06134667963492219933 ) ) ;
#8518=AXIS2_PLACEMENT_3D ( 'NONE', #11123, #3433, #10886 ) ;
#8521=CARTESIAN_POINT ( 'NONE',  ( -0.1116596296178199582, 0.01517857133102903239, -0.3436530038418508792 ) ) ;
#8529=CYLINDRICAL_SURFACE ( 'NONE', #12534, 0.4000000000000000222 ) ;
#8531=CARTESIAN_POINT ( 'NONE',  ( 0.2233192592356399997, 0.1651785713310289783, -0.3073725909049500049 ) ) ;
#8538=CARTESIAN_POINT ( 'NONE',  ( 0.2472135954999579721, 0.3392857142857140795, -0.3402603233408159622 ) ) ;
#8546=CARTESIAN_POINT ( 'NONE',  ( 0.3613381517857143232, -0.05625000009754237834, -0.1174058825155740587 ) ) ;
#8568=EDGE_CURVE ( 'NONE', #20678, #10349, #5714, .T. ) ;
#8573=CARTESIAN_POINT ( 'NONE',  ( 2.326421213736078119E-17, 0.2973214284738861513, -0.3799334167787516425 ) ) ;
#8601=ORIENTED_EDGE ( 'NONE', *, *, #1259, .T. ) ;
#8606=CARTESIAN_POINT ( 'NONE',  ( 4.113055369932088708E-16, 0.1589285712334866096, 0.4000000000000000222 ) ) ;
#8624=CARTESIAN_POINT ( 'NONE',  ( -0.3613381517857144343, 0.1758928570453146822, 0.1174058825155740171 ) ) ;
#8632=CARTESIAN_POINT ( 'NONE',  ( 0.2472135954999579166, 0.1035714285714285227, 0.3402603233408160732 ) ) ;
#8649=CARTESIAN_POINT ( 'NONE',  ( 0.2923287055106771337, 0.004464285616743311064, 0.2123892367102621359 ) ) ;
#8651=LINE ( 'NONE', #19757, #15613 ) ;
#8662=CARTESIAN_POINT ( 'NONE',  ( 0.3613381517857143232, -0.05982142866897095096, 0.000000000000000000 ) ) ;
#8684=DIRECTION ( 'NONE',  ( -0.000000000000000000, -1.000000000000000000, -0.000000000000000000 ) ) ;
#8686=CARTESIAN_POINT ( 'NONE',  ( -0.3999999999999999667, -0.06785714285714286587, -0.1299678784931626030 ) ) ;
#8714=CARTESIAN_POINT ( 'NONE',  ( -0.06335377612981497875, 0.3482590814838159021, -0.3999999999999999667 ) ) ;
#8721=DIRECTION ( 'NONE',  ( 0.000000000000000000, 1.000000000000000000, 0.000000000000000000 ) ) ;
#8730=( BOUNDED_CURVE ( )  B_SPLINE_CURVE ( 2, ( #12789, #11064, #16307, #1551, #8987, #1788, #16550, #22028, #7043, #16432, #23842, #7162, #5325 ),
 .UNSPECIFIED., .F., .F. ) 
 B_SPLINE_CURVE_WITH_KNOTS ( ( 3, 2, 2, 2, 2, 2, 3 ),
 ( 0.2500000000000000000, 0.2571428571428571175, 0.2714285714285714080, 0.2857142857142856984, 0.2999999999999999889, 0.3142857142857142794, 0.3214285714285714524 ),
 .UNSPECIFIED. ) 
 CURVE ( )  GEOMETRIC_REPRESENTATION_ITEM ( )  RATIONAL_B_SPLINE_CURVE ( ( 0.9755282581475768211, 0.9755282581475768211, 1.000000000000000000, 0.9510565162951535312, 1.000000000000000000, 0.9510565162951535312, 1.000000000000000000, 0.9510565162951535312, 1.000000000000000000, 0.9510565162951535312, 1.000000000000000000, 0.9755282581475765991, 0.9755282581475767101 ) ) 
 REPRESENTATION_ITEM ( '' )  );
#8734=ORIENTED_EDGE ( 'NONE', *, *, #21743, .F. ) ;
#8736=CARTESIAN_POINT ( 'NONE',  ( 0.3613381517857143232, 0.2116071427596004084, -0.1174058825155740587 ) ) ;
#8770=CARTESIAN_POINT ( 'NONE',  ( 0.1116596296178199860, 0.09732142847388616791, -0.3436530038418508792 ) ) ;
#8784=CARTESIAN_POINT ( 'NONE',  ( 0.2233192592356399164, 0.07232142847388618734, 0.3073725909049500604 ) ) ;
#8802=EDGE_CURVE ( 'NONE', #17046, #22531, #12869, .T. ) ;
#8806=LINE ( 'NONE', #16012, #5709 ) ;
#8808=CARTESIAN_POINT ( 'NONE',  ( 0.3236067977499790249, 0.04999999999999996114, -0.2351141009169892826 ) ) ;
#8827=VERTEX_POINT ( 'NONE', #21691 ) ;
#8833=CIRCLE ( 'NONE', #3388, 0.09499999999999995948 ) ;
#8837=CARTESIAN_POINT ( 'NONE',  ( -0.1236067977499789583, 0.3499999999999998668, -0.3804226065180614791 ) ) ;
#8844=ORIENTED_EDGE ( 'NONE', *, *, #17678, .F. ) ;
#8859=CARTESIAN_POINT ( 'NONE',  ( 0.2923287055106771337, 0.4330357141881717720, 0.2123892367102621359 ) ) ;
#8864=CARTESIAN_POINT ( 'NONE',  ( -0.1116596296178199582, 0.2294642856167432854, -0.3436530038418508792 ) ) ;
#8867=AXIS2_PLACEMENT_3D ( 'NONE', #14530, #5245, #18302 ) ;
#8882=CARTESIAN_POINT ( 'NONE',  ( -0.2472135954999579444, 0.2107142857142856318, -0.3402603233408160732 ) ) ;
#8883=APPLICATION_CONTEXT ( 'configuration controlled 3d designs of mechanical parts and assemblies' ) ;
#8885=B_SPLINE_CURVE_WITH_KNOTS ( 'NONE', 3,
 ( #20491, #3787, #11231, #1953, #16837, #121, #7564, #6450, #12206, #13674, #8515, #17791, #8274, #21449, #13781, #15840, #2677, #22914, #846, #21331, #17672, #17552 ),
 .UNSPECIFIED., .F., .F.,
 ( 4, 2, 2, 2, 2, 2, 2, 2, 2, 2, 4 ),
 ( 0.000000000000000000, 0.001811609990388479826, 0.003623219980776959653, 0.004529024975971198373, 0.005434829971165437527, 0.007246439961553915836, 0.009058049951942395012, 0.009963854947136637635, 0.01086965994233087852, 0.01268126993271936377, 0.01449287992310785075 ),
 .UNSPECIFIED. ) ;
#8897=CARTESIAN_POINT ( 'NONE',  ( 0.2923287055106771337, 0.09017857133102899492, -0.2123892367102620249 ) ) ;
#8907=CARTESIAN_POINT ( 'NONE',  ( -0.1236067977499789583, 0.06428571428571425161, -0.3804226065180614791 ) ) ;
#8912=CARTESIAN_POINT ( 'NONE',  ( -0.2923287055106771337, 0.1116071427596004445, -0.2123892367102620804 ) ) ;
#8916=CARTESIAN_POINT ( 'NONE',  ( 0.000000000000000000, 3.700000000000000622, 0.000000000000000000 ) ) ;
#8929=EDGE_LOOP ( 'NONE', ( #8958, #12524, #7489, #14752 ) ) ;
#8933=CARTESIAN_POINT ( 'NONE',  ( -0.1236067977499789583, -0.07857142857142858372, -0.3804226065180614791 ) ) ;
#8934=CYLINDRICAL_SURFACE ( 'NONE', #24081, 0.4000000000000000222 ) ;
#8958=ORIENTED_EDGE ( 'NONE', *, *, #13984, .F. ) ;
#8960=CIRCLE ( 'NONE', #1937, 0.7500000000000001110 ) ;
#8964=CARTESIAN_POINT ( 'NONE',  ( -7.000945310522701902E-17, 0.3821428571428570620, 0.3999999999999999667 ) ) ;
#8983=( BOUNDED_SURFACE ( )  B_SPLINE_SURFACE ( 1, 2, ( 
 ( #15384, #12338, #3407, #4989, #16098, #19755, #3282, #14513, #20116, #21464, #16340, #1462, #23512, #5107, #21577, #23635, #10497, #6585, #8649, #12453, #1340, #14391, #21934, #5227, #23396, #4872, #21817, #3050, #6703, #6828, #19872, #6952, #17927, #18165, #1223, #12573, #19994, #14148, #10857, #4748, #12701, #979, #8897, #8406, #8770, #10736, #1099, #14268, #23753, #7075, #21705, #3164, #15856, #10614, #18044, #16222, #23273, #14034, #12219, #19629, #2927, #10386, #17808, #8531, #15975, #5479, #15119, #9019, #7433, #16935, #233, #2060, #13299, #18524, #11215, #24001, #16460, #12944, #7313, #1813, #14763, #9258, #12820, #22545, #5354, #22421, #1698, #10979, #5722, #20714, #13059, #18285, #18644, #5594, #7668, #16699, #20356, #1936, #14880, #9501, #3528, #5835, #1583, #4010, #11093, #23872, #13182, #24118, #9384, #7192, #22297, #20477, #20595, #18405, #22178, #20238, #14637, #3646, #22059, #3772, #16824, #106, #9135, #3890, #7547, #14999, #16580, #11336, #18765, #13539, #4126, #18891, #20954, #22780, #9869, #17296, #6192, #21073, #17182, #22898, #710 ),
 ( #2662, #13657, #17536, #8021, #4248, #6074, #8258, #2192, #589, #10112, #829, #19363, #6433, #11699, #4363, #468, #9623, #19123, #7899, #2427, #15351, #15471, #5952, #15708, #22663, #15588, #19012, #11582, #23012, #13887, #11821, #11458, #19240, #2544, #23122, #9992, #17416, #8138, #6314, #21314, #20834, #17056, #349, #7789, #13766, #15234, #13411, #21192, #4483, #11950, #2308, #9745, #3137, #23721, #1435, #21547, #8498, #14118, #10226, #17654, #23605, #3252, #10468, #15822, #17774, #21673, #4958, #15938, #16069, #23363, #7045, #8624, #19718, #6673, #6919, #18138, #14482, #941, #19965, #5076, #3020, #8736, #1067, #10587, #4836, #8371, #8864, #23241, #12304, #16308, #14358, #6550, #23481, #12425, #19595, #17897, #6798, #1312, #14236, #16192, #19838, #21788, #1191, #2774, #18014, #4605, #14000, #12067, #12545, #19480, #10703, #2890, #21433, #10350, #4718, #12191, #5568, #7643, #12667, #16794, #13033, #20210, #7284, #23843, #14734, #24095, #201, #16433, #12790, #7405, #18494, #16552, #20087, #16906, #5196, #9474, #9102, #7163, #3745, #12912, #23973 ) ),
 .UNSPECIFIED., .F., .F., .T. ) 
 B_SPLINE_SURFACE_WITH_KNOTS ( ( 2, 2 ),
 ( 3, 2, 2, 2, 2, 2, 2, 2, 2, 2, 2, 2, 2, 2, 2, 2, 2, 2, 2, 2, 2, 2, 2, 2, 2, 2, 2, 2, 2, 2, 2, 2, 2, 2, 2, 2, 2, 2, 2, 2, 2, 2, 2, 2, 2, 2, 2, 2, 2, 2, 2, 2, 2, 2, 2, 2, 2, 2, 2, 2, 2, 2, 2, 2, 2, 2, 2, 2, 2, 2, 3 ),
 ( 0.000000000000000000, 1.000000000000000000 ),
 ( 0.000000000000000000, 0.01428571428571428527, 0.02857142857142857054, 0.04285714285714285754, 0.05714285714285714107, 0.07142857142857142461, 0.08571428571428571508, 0.1000000000000000056, 0.1142857142857142821, 0.1285714285714285587, 0.1428571428571428492, 0.1571428571428571397, 0.1714285714285714302, 0.1857142857142857206, 0.2000000000000000111, 0.2142857142857142738, 0.2285714285714285643, 0.2428571428571428548, 0.2571428571428571175, 0.2714285714285714080, 0.2857142857142856984, 0.2999999999999999889, 0.3142857142857142794, 0.3285714285714285698, 0.3428571428571428603, 0.3571428571428571508, 0.3714285714285714413, 0.3857142857142857317, 0.4000000000000000222, 0.4142857142857143127, 0.4285714285714285476, 0.4428571428571428381, 0.4571428571428571286, 0.4714285714285714191, 0.4857142857142857095, 0.5000000000000000000, 0.5142857142857142350, 0.5285714285714285809, 0.5428571428571428159, 0.5571428571428571619, 0.5714285714285713969, 0.5857142857142857428, 0.5999999999999999778, 0.6142857142857143238, 0.6285714285714285587, 0.6428571428571429047, 0.6571428571428571397, 0.6714285714285713746, 0.6857142857142857206, 0.6999999999999999556, 0.7142857142857143016, 0.7285714285714285365, 0.7428571428571428825, 0.7571428571428571175, 0.7714285714285714635, 0.7857142857142856984, 0.8000000000000000444, 0.8142857142857142794, 0.8285714285714286254, 0.8428571428571428603, 0.8571428571428570953, 0.8714285714285714413, 0.8857142857142856762, 0.9000000000000000222, 0.9142857142857142572, 0.9285714285714286031, 0.9428571428571428381, 0.9571428571428571841, 0.9714285714285714191, 0.9857142857142857650, 1.000000000000000000 ),
 .UNSPECIFIED. ) 
 GEOMETRIC_REPRESENTATION_ITEM ( )  RATIONAL_B_SPLINE_SURFACE ( (
 ( 1.000000000000000000, 0.9510565162951535312, 1.000000000000000000, 0.9510565162951535312, 1.000000000000000000, 0.9510565162951535312, 1.000000000000000000, 0.9510565162951535312, 1.000000000000000000, 0.9510565162951535312, 1.000000000000000000, 0.9510565162951535312, 1.000000000000000000, 0.9510565162951535312, 1.000000000000000000, 0.9510565162951535312, 1.000000000000000000, 0.9510565162951535312, 1.000000000000000000, 0.9510565162951535312, 1.000000000000000000, 0.9510565162951535312, 1.000000000000000000, 0.9510565162951535312, 1.000000000000000000, 0.9510565162951535312, 1.000000000000000000, 0.9510565162951535312, 1.000000000000000000, 0.9510565162951535312, 1.000000000000000000, 0.9510565162951535312, 1.000000000000000000, 0.9510565162951535312, 1.000000000000000000, 0.9510565162951535312, 1.000000000000000000, 0.9510565162951535312, 1.000000000000000000, 0.9510565162951535312, 1.000000000000000000, 0.9510565162951535312, 1.000000000000000000, 0.9510565162951535312, 1.000000000000000000, 0.9510565162951535312, 1.000000000000000000, 0.9510565162951535312, 1.000000000000000000, 0.9510565162951535312, 1.000000000000000000, 0.9510565162951535312, 1.000000000000000000, 0.9510565162951535312, 1.000000000000000000, 0.9510565162951535312, 1.000000000000000000, 0.9510565162951535312, 1.000000000000000000, 0.9510565162951535312, 1.000000000000000000, 0.9510565162951535312, 1.000000000000000000, 0.9510565162951535312, 1.000000000000000000, 0.9510565162951535312, 1.000000000000000000, 0.9510565162951535312, 1.000000000000000000, 0.9510565162951535312, 1.000000000000000000, 0.9510565162951535312, 1.000000000000000000, 0.9510565162951535312, 1.000000000000000000, 0.9510565162951535312, 1.000000000000000000, 0.9510565162951535312, 1.000000000000000000, 0.9510565162951535312, 1.000000000000000000, 0.9510565162951535312, 1.000000000000000000, 0.9510565162951535312, 1.000000000000000000, 0.9510565162951535312, 1.000000000000000000, 0.9510565162951535312, 1.000000000000000000, 0.9510565162951535312, 1.000000000000000000, 0.9510565162951535312, 1.000000000000000000, 0.9510565162951535312, 1.000000000000000000, 0.9510565162951535312, 1.000000000000000000, 0.9510565162951535312, 1.000000000000000000, 0.9510565162951535312, 1.000000000000000000, 0.9510565162951535312, 1.000000000000000000, 0.9510565162951535312, 1.000000000000000000, 0.9510565162951535312, 1.000000000000000000, 0.9510565162951535312, 1.000000000000000000, 0.9510565162951535312, 1.000000000000000000, 0.9510565162951535312, 1.000000000000000000, 0.9510565162951535312, 1.000000000000000000, 0.9510565162951535312, 1.000000000000000000, 0.9510565162951535312, 1.000000000000000000, 0.9510565162951535312, 1.000000000000000000, 0.9510565162951535312, 1.000000000000000000, 0.9510565162951535312, 1.000000000000000000, 0.9510565162951535312, 1.000000000000000000, 0.9510565162951535312, 1.000000000000000000, 0.9510565162951535312, 1.000000000000000000, 0.9510565162951535312, 1.000000000000000000, 0.9510565162951535312, 1.000000000000000000, 0.9510565162951535312, 1.000000000000000000, 0.9510565162951535312, 1.000000000000000000, 0.9510565162951535312, 1.000000000000000000),
 ( 1.000000000000000000, 0.9510565162951535312, 1.000000000000000000, 0.9510565162951535312, 1.000000000000000000, 0.9510565162951535312, 1.000000000000000000, 0.9510565162951535312, 1.000000000000000000, 0.9510565162951535312, 1.000000000000000000, 0.9510565162951535312, 1.000000000000000000, 0.9510565162951535312, 1.000000000000000000, 0.9510565162951535312, 1.000000000000000000, 0.9510565162951535312, 1.000000000000000000, 0.9510565162951535312, 1.000000000000000000, 0.9510565162951535312, 1.000000000000000000, 0.9510565162951535312, 1.000000000000000000, 0.9510565162951535312, 1.000000000000000000, 0.9510565162951535312, 1.000000000000000000, 0.9510565162951535312, 1.000000000000000000, 0.9510565162951535312, 1.000000000000000000, 0.9510565162951535312, 1.000000000000000000, 0.9510565162951535312, 1.000000000000000000, 0.9510565162951535312, 1.000000000000000000, 0.9510565162951535312, 1.000000000000000000, 0.9510565162951535312, 1.000000000000000000, 0.9510565162951535312, 1.000000000000000000, 0.9510565162951535312, 1.000000000000000000, 0.9510565162951535312, 1.000000000000000000, 0.9510565162951535312, 1.000000000000000000, 0.9510565162951535312, 1.000000000000000000, 0.9510565162951535312, 1.000000000000000000, 0.9510565162951535312, 1.000000000000000000, 0.9510565162951535312, 1.000000000000000000, 0.9510565162951535312, 1.000000000000000000, 0.9510565162951535312, 1.000000000000000000, 0.9510565162951535312, 1.000000000000000000, 0.9510565162951535312, 1.000000000000000000, 0.9510565162951535312, 1.000000000000000000, 0.9510565162951535312, 1.000000000000000000, 0.9510565162951535312, 1.000000000000000000, 0.9510565162951535312, 1.000000000000000000, 0.9510565162951535312, 1.000000000000000000, 0.9510565162951535312, 1.000000000000000000, 0.9510565162951535312, 1.000000000000000000, 0.9510565162951535312, 1.000000000000000000, 0.9510565162951535312, 1.000000000000000000, 0.9510565162951535312, 1.000000000000000000, 0.9510565162951535312, 1.000000000000000000, 0.9510565162951535312, 1.000000000000000000, 0.9510565162951535312, 1.000000000000000000, 0.9510565162951535312, 1.000000000000000000, 0.9510565162951535312, 1.000000000000000000, 0.9510565162951535312, 1.000000000000000000, 0.9510565162951535312, 1.000000000000000000, 0.9510565162951535312, 1.000000000000000000, 0.9510565162951535312, 1.000000000000000000, 0.9510565162951535312, 1.000000000000000000, 0.9510565162951535312, 1.000000000000000000, 0.9510565162951535312, 1.000000000000000000, 0.9510565162951535312, 1.000000000000000000, 0.9510565162951535312, 1.000000000000000000, 0.9510565162951535312, 1.000000000000000000, 0.9510565162951535312, 1.000000000000000000, 0.9510565162951535312, 1.000000000000000000, 0.9510565162951535312, 1.000000000000000000, 0.9510565162951535312, 1.000000000000000000, 0.9510565162951535312, 1.000000000000000000, 0.9510565162951535312, 1.000000000000000000, 0.9510565162951535312, 1.000000000000000000, 0.9510565162951535312, 1.000000000000000000, 0.9510565162951535312, 1.000000000000000000, 0.9510565162951535312, 1.000000000000000000, 0.9510565162951535312, 1.000000000000000000, 0.9510565162951535312, 1.000000000000000000) ) ) 
 REPRESENTATION_ITEM ( '' )  SURFACE ( )  );
#8985=CARTESIAN_POINT ( 'NONE',  ( -0.2233192592356399442, 0.3937499999024575148, -0.3073725909049500049 ) ) ;
#8987=CARTESIAN_POINT ( 'NONE',  ( 0.3236067977499789694, 0.03571428571428568455, 0.2351141009169893659 ) ) ;
#9019=CARTESIAN_POINT ( 'NONE',  ( -0.2233192592356399442, 0.1794642856167432965, -0.3073725909049500049 ) ) ;
#9022=CARTESIAN_POINT ( 'NONE',  ( 0.3999999999999999667, 0.03749999980491518919, -0.1299678784931625197 ) ) ;
#9032=CARTESIAN_POINT ( 'NONE',  ( -0.3613381517857143232, 0.1866071427596003862, -0.1174058825155741004 ) ) ;
#9038=CARTESIAN_POINT ( 'NONE',  ( -7.000945310522701902E-17, 0.3821428571428570620, 0.3999999999999999667 ) ) ;
#9042=CARTESIAN_POINT ( 'NONE',  ( 0.3236067977499790249, 0.1928571428571428104, -0.2351141009169892826 ) ) ;
#9052=CARTESIAN_POINT ( 'NONE',  ( -0.2233192592356399997, 0.3973214284738861291, 0.3073725909049499494 ) ) ;
#9058=CARTESIAN_POINT ( 'NONE',  ( -0.4000000000000000222, 0.001785714090629508333, 0.1299678784931624920 ) ) ;
#9082=CARTESIAN_POINT ( 'NONE',  ( -0.2233192592356399442, 0.03660714275960045422, -0.3073725909049499494 ) ) ;
#9097=ORIENTED_EDGE ( 'NONE', *, *, #17829, .F. ) ;
#9102=CARTESIAN_POINT ( 'NONE',  ( 0.1116596296178199027, 0.4080357141881718608, 0.3436530038418508792 ) ) ;
#9126=( BOUNDED_CURVE ( )  B_SPLINE_CURVE ( 2, ( #17033, #13518, #2040, #565, #14974, #6171, #4226, #4102, #3871, #22396, #9723, #19102, #18866 ),
 .UNSPECIFIED., .F., .F. ) 
 B_SPLINE_CURVE_WITH_KNOTS ( ( 3, 2, 2, 2, 2, 2, 3 ),
 ( 0.8928571428571429047, 0.9000000000000000222, 0.9142857142857142572, 0.9285714285714286031, 0.9428571428571428381, 0.9571428571428571841, 0.9642857142857143016 ),
 .UNSPECIFIED. ) 
 CURVE ( )  GEOMETRIC_REPRESENTATION_ITEM ( )  RATIONAL_B_SPLINE_CURVE ( ( 0.9755282581475768211, 0.9755282581475769321, 1.000000000000000000, 0.9510565162951535312, 1.000000000000000000, 0.9510565162951535312, 1.000000000000000000, 0.9510565162951535312, 1.000000000000000000, 0.9510565162951535312, 1.000000000000000000, 0.9755282581475768211, 0.9755282581475768211 ) ) 
 REPRESENTATION_ITEM ( '' )  );
#9127=AXIS2_PLACEMENT_3D ( 'NONE', #15878, #23181, #23294 ) ;
#9135=CARTESIAN_POINT ( 'NONE',  ( 0.2923287055106771337, 0.3758928570453146656, -0.2123892367102620249 ) ) ;
#9150=CARTESIAN_POINT ( 'NONE',  ( -6.979263641208234666E-17, 0.2080357141881718497, 0.3799334167787516425 ) ) ;
#9154=ORIENTED_EDGE ( 'NONE', *, *, #22688, .F. ) ;
#9160=CARTESIAN_POINT ( 'NONE',  ( 0.1236067977499789028, 0.1714285714285714024, 0.3804226065180614791 ) ) ;
#9167=EDGE_LOOP ( 'NONE', ( #6635, #6759, #13212, #9639 ) ) ;
#9173=CARTESIAN_POINT ( 'NONE',  ( 2.575339694675500462E-17, 0.06071428571428567206, -0.4205848896953069405 ) ) ;
#9178=EDGE_CURVE ( 'NONE', #22290, #2118, #16925, .T. ) ;
#9179=ADVANCED_FACE ( 'NONE', ( #9615 ), #578, .T. ) ;
#9181=CARTESIAN_POINT ( 'NONE',  ( 0.3999999999999999667, 0.03035714266205807518, 0.1299678784931626307 ) ) ;
#9206=FACE_OUTER_BOUND ( 'NONE', #4312, .T. ) ;
#9209=CARTESIAN_POINT ( 'NONE',  ( 0.1116596296178199860, 0.02589285704531474330, -0.3436530038418508792 ) ) ;
#9213=LINE ( 'NONE', #21889, #2942 ) ;
#9236=DIRECTION ( 'NONE',  ( 1.000000000000000000, 0.000000000000000000, 0.000000000000000000 ) ) ;
#9258=CARTESIAN_POINT ( 'NONE',  ( 0.3613381517857143232, 0.2294642856167432576, -0.1174058825155740587 ) ) ;
#9271=CARTESIAN_POINT ( 'NONE',  ( -0.2923287055106771337, 0.1830357141881718552, -0.2123892367102620804 ) ) ;
#9292=CARTESIAN_POINT ( 'NONE',  ( -0.2472135954999579999, 0.2321428571428570675, 0.3402603233408159622 ) ) ;
#9294=EDGE_CURVE ( 'NONE', #16753, #15714, #8960, .T. ) ;
#9300=CARTESIAN_POINT ( 'NONE',  ( -0.4000000000000000222, -0.001785714480799064936, -4.898587196589413075E-17 ) ) ;
#9328=ORIENTED_EDGE ( 'NONE', *, *, #14352, .T. ) ;
#9329=CARTESIAN_POINT ( 'NONE',  ( 2.326421213736078119E-17, 0.1723214284738861790, -0.3799334167787516980 ) ) ;
#9343=CARTESIAN_POINT ( 'NONE',  ( -0.1116596296178199582, 0.08660714275960045005, -0.3436530038418508792 ) ) ;
#9347=AXIS2_PLACEMENT_3D ( 'NONE', #3764, #2417, #6064 ) ;
#9361=CARTESIAN_POINT ( 'NONE',  ( -0.2472135954999579999, 0.08035714266205803979, 0.3402603233408160732 ) ) ;
#9362=AXIS2_PLACEMENT_3D ( 'NONE', #1047, #15915, #4940 ) ;
#9378=AXIS2_PLACEMENT_3D ( 'NONE', #22794, #23924, #19136 ) ;
#9384=CARTESIAN_POINT ( 'NONE',  ( -0.2923287055106771337, 0.3258928570453146767, -0.2123892367102620804 ) ) ;
#9394=CARTESIAN_POINT ( 'NONE',  ( 0.2233192592356399164, 0.1437499999024575981, 0.3073725909049500604 ) ) ;
#9397=CARTESIAN_POINT ( 'NONE',  ( 0.4000000000000000222, 0.3910714283763437327, 0.000000000000000000 ) ) ;
#9399=ORIENTED_EDGE ( 'NONE', *, *, #18211, .F. ) ;
#9409=DIRECTION ( 'NONE',  ( 0.000000000000000000, 0.000000000000000000, 1.000000000000000000 ) ) ;
#9411=EDGE_LOOP ( 'NONE', ( #9154, #17982, #3854, #19272 ) ) ;
#9415=CARTESIAN_POINT ( 'NONE',  ( -0.4000000000000000222, 0.3553571426620580342, -4.898587196589413075E-17 ) ) ;
#9416=CARTESIAN_POINT ( 'NONE',  ( 0.1236067977499789028, 0.3142857142857142239, 0.3804226065180614791 ) ) ;
#9423=CARTESIAN_POINT ( 'NONE',  ( -0.4000000000000000222, 0.1446428569477723469, 0.1299678784931624920 ) ) ;
#9443=ORIENTED_EDGE ( 'NONE', *, *, #18738, .T. ) ;
#9446=CARTESIAN_POINT ( 'NONE',  ( 0.3613381517857143232, -0.009821428668970965531, 0.1174058825155742114 ) ) ;
#9449=CARTESIAN_POINT ( 'NONE',  ( -0.1116596296178199582, 0.03303571418817188854, -0.3436530038418508792 ) ) ;
#9463=ORIENTED_EDGE ( 'NONE', *, *, #4838, .T. ) ;
#9466=VERTEX_POINT ( 'NONE', #14725 ) ;
#9472=ADVANCED_FACE ( 'NONE', ( #20200 ), #22019, .T. ) ;
#9473=B_SPLINE_CURVE_WITH_KNOTS ( 'NONE', 3,
 ( #719, #15360, #7471, #4257, #6082, #9877, #11708, #17306, #9753, #19489, #17190, #19374, #19131, #2435, #2671, #16742, #4372, #24, #8147, #6202, #839, #13668, #14920, #599, #8030, #21082 ),
 .UNSPECIFIED., .F., .F.,
 ( 4, 2, 2, 2, 2, 2, 2, 2, 2, 2, 2, 2, 4 ),
 ( 0.000000000000000000, 0.002383362014287317403, 0.004766724028574634807, 0.005958405035718294593, 0.007150086042861953511, 0.008341767050005612430, 0.009533448057149271349, 0.01191681007143659092, 0.01310849107858024984, 0.01430017208572390702, 0.01549185309286757115, 0.01668353410001123527, 0.01906689611429856004 ),
 .UNSPECIFIED. ) ;
#9474=CARTESIAN_POINT ( 'NONE',  ( -6.979263641208234666E-17, 0.4044642856167431355, 0.3799334167787516425 ) ) ;
#9481=CARTESIAN_POINT ( 'NONE',  ( 1.750236327630675475E-17, 0.05178571409062948661, -0.3999999999999999667 ) ) ;
#9501=CARTESIAN_POINT ( 'NONE',  ( 0.3613381517857143232, 0.2937499999024575370, 0.1174058825155742114 ) ) ;
#9507=AXIS2_PLACEMENT_3D ( 'NONE', #4370, #717, #15597 ) ;
#9514=CARTESIAN_POINT ( 'NONE',  ( 0.3236067977499789694, 0.3839285712334865597, 0.2351141009169893659 ) ) ;
#9516=ORIENTED_EDGE ( 'NONE', *, *, #2272, .T. ) ;
#9531=ORIENTED_EDGE ( 'NONE', *, *, #14815, .T. ) ;
#9535=CARTESIAN_POINT ( 'NONE',  ( 2.575339694675500462E-17, 0.2035714285714285143, -0.4205848896953069405 ) ) ;
#9542=CARTESIAN_POINT ( 'NONE',  ( 0.1236067977499789028, 0.1624999998049152239, 0.3804226065180614791 ) ) ;
#9566=CARTESIAN_POINT ( 'NONE',  ( -0.2233192592356399442, 0.09017857133102905043, -0.3073725909049500049 ) ) ;
#9570=CARTESIAN_POINT ( 'NONE',  ( -0.2233192592356400275, 0.2008928570453147322, 0.3073725909049499494 ) ) ;
#9584=CARTESIAN_POINT ( 'NONE',  ( 0.3613381517857143232, 0.06517857133102902822, 0.000000000000000000 ) ) ;
#9587=ORIENTED_EDGE ( 'NONE', *, *, #14542, .T. ) ;
#9602=ADVANCED_FACE ( 'NONE', ( #12906 ), #20319, .T. ) ;
#9615=FACE_OUTER_BOUND ( 'NONE', #24054, .T. ) ;
#9623=CARTESIAN_POINT ( 'NONE',  ( 0.1116596296178199027, -0.02053571438325667992, 0.3436530038418508792 ) ) ;
#9630=( BOUNDED_CURVE ( )  B_SPLINE_CURVE ( 2, ( #10145, #17569, #859, #15744, #4636, #12102, #6102, #19512, #2805, #10260, #7819, #15262, #5981 ),
 .UNSPECIFIED., .F., .T. ) 
 B_SPLINE_CURVE_WITH_KNOTS ( ( 3, 2, 2, 2, 2, 2, 3 ),
 ( 0.6785714285714286031, 0.6857142857142857206, 0.6999999999999999556, 0.7142857142857143016, 0.7285714285714285365, 0.7428571428571428825, 0.7500000000000000000 ),
 .UNSPECIFIED. ) 
 CURVE ( )  GEOMETRIC_REPRESENTATION_ITEM ( )  RATIONAL_B_SPLINE_CURVE ( ( 0.9755282581475768211, 0.9755282581475769321, 1.000000000000000000, 0.9510565162951535312, 1.000000000000000000, 0.9510565162951535312, 1.000000000000000000, 0.9510565162951535312, 1.000000000000000000, 0.9510565162951535312, 1.000000000000000000, 0.9755282581475768211, 0.9755282581475768211 ) ) 
 REPRESENTATION_ITEM ( '' )  );
#9639=ORIENTED_EDGE ( 'NONE', *, *, #17817, .F. ) ;
#9642=CARTESIAN_POINT ( 'NONE',  ( 0.2923287055106771337, 0.4151785713310289228, 0.2123892367102621359 ) ) ;
#9657=CARTESIAN_POINT ( 'NONE',  ( -0.1236067977499789583, 0.2785714285714285254, -0.3804226065180614791 ) ) ;
#9665=TOROIDAL_SURFACE ( 'NONE', #5763, 0.3425000000000000266, 0.02999999999999999889 ) ;
#9666=CARTESIAN_POINT ( 'NONE',  ( 2.575339694675500462E-17, 0.4089285712334865264, -0.4205848896953069405 ) ) ;
#9687=PLANE ( 'NONE',  #10520 ) ;
#9688=CARTESIAN_POINT ( 'NONE',  ( -0.1116596296178199582, -0.05625000009754239222, -0.3436530038418508792 ) ) ;
#9692=CARTESIAN_POINT ( 'NONE',  ( -0.3613381517857143788, 0.2651785713310289561, 0.1174058825155740310 ) ) ;
#9705=CARTESIAN_POINT ( 'NONE',  ( -0.2923287055106771337, 0.1080357141881718719, 0.2123892367102619971 ) ) ;
#9712=CARTESIAN_POINT ( 'NONE',  ( 0.000000000000000000, 3.659999999999999698, 0.000000000000000000 ) ) ;
#9723=CARTESIAN_POINT ( 'NONE',  ( -0.1236067977499790416, 0.4410714283763437216, 0.3804226065180614236 ) ) ;
#9727=CARTESIAN_POINT ( 'NONE',  ( -0.2232596883534626875, -3.892158461848153852E-18, 0.3143945333366566230 ) ) ;
#9731=CARTESIAN_POINT ( 'NONE',  ( -0.1236067977499790416, 0.2357142857142856818, 0.3804226065180614236 ) ) ;
#9745=CARTESIAN_POINT ( 'NONE',  ( -0.3613381517857144343, 0.1044642856167432993, 0.1174058825155740171 ) ) ;
#9753=CARTESIAN_POINT ( 'NONE',  ( -0.1023465816611775492, 2.632010880910606029E-18, -0.3732753122504546273 ) ) ;
#9760=EDGE_CURVE ( 'NONE', #14906, #13117, #22377, .T. ) ;
#9765=CARTESIAN_POINT ( 'NONE',  ( 0.2923287055106771337, 0.3437499999024575814, 0.2123892367102621359 ) ) ;
#9771=DIRECTION ( 'NONE',  ( 0.000000000000000000, 1.000000000000000000, 0.000000000000000000 ) ) ;
#9780=ORIENTED_EDGE ( 'NONE', *, *, #7098, .F. ) ;
#9784=CARTESIAN_POINT ( 'NONE',  ( 0.2472135954999579166, 0.2464285714285713302, 0.3402603233408160732 ) ) ;
#9792=VECTOR ( 'NONE', #20042, 39.37007874015748143 ) ;
#9794=CARTESIAN_POINT ( 'NONE',  ( 0.4000000000000000222, 0.3196428569477723358, 0.000000000000000000 ) ) ;
#9801=CARTESIAN_POINT ( 'NONE',  ( -0.4000000000000000222, 0.2839285712334865819, -4.898587196589413075E-17 ) ) ;
#9806=CARTESIAN_POINT ( 'NONE',  ( 0.4000000000000000222, 0.4624999998049150740, 0.000000000000000000 ) ) ;
#9814=CARTESIAN_POINT ( 'NONE',  ( 0.3613381517857143232, 0.1401785713310289838, -0.1174058825155740587 ) ) ;
#9815=CARTESIAN_POINT ( 'NONE',  ( -4.638126268221291196E-16, 0.1321428571428571175, -0.4000000000000000222 ) ) ;
#9830=CARTESIAN_POINT ( 'NONE',  ( -0.2233192592356400275, 0.04017857133102901990, 0.3073725909049499494 ) ) ;
#9856=CARTESIAN_POINT ( 'NONE',  ( -0.3236067977499789694, 0.2857142857142855874, -0.2351141009169893104 ) ) ;
#9868=ADVANCED_FACE ( 'NONE', ( #5516 ), #5271, .F. ) ;
#9869=CARTESIAN_POINT ( 'NONE',  ( -0.1116596296178200276, 0.4187499999024575370, 0.3436530038418508792 ) ) ;
#9875=FACE_OUTER_BOUND ( 'NONE', #14544, .T. ) ;
#9877=CARTESIAN_POINT ( 'NONE',  ( -0.1622275593423418982, 1.937136306180702348E-16, -0.3548286843789034140 ) ) ;
#9889=CARTESIAN_POINT ( 'NONE',  ( -0.2233192592356399442, 0.3758928570453146656, -0.3073725909049499494 ) ) ;
#9909=CARTESIAN_POINT ( 'NONE',  ( 0.1236067977499789028, 0.2339285712334865930, 0.3804226065180614791 ) ) ;
#9926=ORIENTED_EDGE ( 'NONE', *, *, #7985, .F. ) ;
#9934=CARTESIAN_POINT ( 'NONE',  ( 0.3613381517857143232, 0.2758928570453146878, 0.1174058825155742114 ) ) ;
#9949=CARTESIAN_POINT ( 'NONE',  ( -6.979263641208234666E-17, 0.2616071427596003973, 0.3799334167787516980 ) ) ;
#9951=ORIENTED_EDGE ( 'NONE', *, *, #4975, .T. ) ;
#9956=CARTESIAN_POINT ( 'NONE',  ( 0.000000000000000000, 3.700000000000000622, 0.000000000000000000 ) ) ;
#9992=CARTESIAN_POINT ( 'NONE',  ( -6.979263641208234666E-17, 0.04732142847388615819, 0.3799334167787516425 ) ) ;
#10037=CARTESIAN_POINT ( 'NONE',  ( -0.2472135954999579999, 0.2232142855192008613, 0.3402603233408159622 ) ) ;
#10057=CARTESIAN_POINT ( 'NONE',  ( -0.2233192592356399442, 0.3758928570453146656, -0.3073725909049500049 ) ) ;
#10059=CARTESIAN_POINT ( 'NONE',  ( -0.2923287055106771337, 0.2687499999024575703, 0.2123892367102619971 ) ) ;
#10071=CONICAL_SURFACE ( 'NONE', #23664, 0.3125000000000000000, 0.7853981633974482790 ) ;
#10072=EDGE_LOOP ( 'NONE', ( #3997, #21954, #23566, #7276 ) ) ;
#10073=CARTESIAN_POINT ( 'NONE',  ( -0.3613381517857143788, 0.2473214284738861068, 0.1174058825155740310 ) ) ;
#10107=AXIS2_PLACEMENT_3D ( 'NONE', #21293, #20036, #4586 ) ;
#10108=ORIENTED_EDGE ( 'NONE', *, *, #10876, .F. ) ;
#10112=CARTESIAN_POINT ( 'NONE',  ( -0.3613381517857143232, -0.04553571438325666049, -0.1174058825155741004 ) ) ;
#10115=CARTESIAN_POINT ( 'NONE',  ( 0.000000000000000000, 3.659999999999999698, 0.000000000000000000 ) ) ;
#10145=CARTESIAN_POINT ( 'NONE',  ( 9.101228903679513089E-16, 0.2392857142857141850, 0.4000000000000000222 ) ) ;
#10149=CARTESIAN_POINT ( 'NONE',  ( 0.4000000000000000222, 0.3285714285714284588, 0.000000000000000000 ) ) ;
#10156=CARTESIAN_POINT ( 'NONE',  ( -0.2472135954999579444, 0.2732142855192009057, -0.3402603233408159622 ) ) ;
#10160=CARTESIAN_POINT ( 'NONE',  ( 0.1236067977499789028, 0.1624999998049151961, 0.3804226065180614791 ) ) ;
#10170=CARTESIAN_POINT ( 'NONE',  ( 0.4000000000000000222, 0.3285714285714284588, 0.000000000000000000 ) ) ;
#10180=CARTESIAN_POINT ( 'NONE',  ( 0.3613381517857143232, 0.3473214284738860291, 0.1174058825155742114 ) ) ;
#10182=CARTESIAN_POINT ( 'NONE',  ( 0.2923287055106771337, 0.4330357141881717720, 0.2123892367102621359 ) ) ;
#10212=FACE_OUTER_BOUND ( 'NONE', #21539, .T. ) ;
#10224=VECTOR ( 'NONE', #15216, 39.37007874015748143 ) ;
#10226=CARTESIAN_POINT ( 'NONE',  ( 0.2923287055106771337, 0.1294642856167433076, 0.2123892367102621359 ) ) ;
#10227=ADVANCED_FACE ( 'NONE', ( #13601 ), #9687, .T. ) ;
#10233=ORIENTED_EDGE ( 'NONE', *, *, #10624, .F. ) ;
#10260=CARTESIAN_POINT ( 'NONE',  ( 0.2472135954999579721, 0.2678571428571427382, -0.3402603233408160732 ) ) ;
#10268=VERTEX_POINT ( 'NONE', #15297 ) ;
#10274=CARTESIAN_POINT ( 'NONE',  ( -0.4000000000000000222, 0.4267857140906294866, -4.898587196589413075E-17 ) ) ;
#10284=DIRECTION ( 'NONE',  ( 0.000000000000000000, 1.000000000000000000, 0.000000000000000000 ) ) ;
#10292=ORIENTED_EDGE ( 'NONE', *, *, #10822, .F. ) ;
#10298=CARTESIAN_POINT ( 'NONE',  ( 0.3613381517857143232, 0.2080357141881718774, 0.000000000000000000 ) ) ;
#10315=AXIS2_PLACEMENT_3D ( 'NONE', #1387, #23438, #14193 ) ;
#10349=VERTEX_POINT ( 'NONE', #19427 ) ;
#10350=CARTESIAN_POINT ( 'NONE',  ( -0.2233192592356399997, 0.3258928570453145657, 0.3073725909049499494 ) ) ;
#10375=EDGE_CURVE ( 'NONE', #4661, #19679, #892, .T. ) ;
#10386=CARTESIAN_POINT ( 'NONE',  ( 0.3613381517857143232, 0.1580357141881718608, -0.1174058825155740587 ) ) ;
#10399=CARTESIAN_POINT ( 'NONE',  ( 0.2233192592356399997, 0.09374999990245759529, -0.3073725909049500049 ) ) ;
#10404=CARTESIAN_POINT ( 'NONE',  ( 0.2472135954999579166, 0.1660714283763436994, 0.3402603233408160732 ) ) ;
#10413=ORIENTED_EDGE ( 'NONE', *, *, #18070, .F. ) ;
#10415=LINE ( 'NONE', #20022, #2390 ) ;
#10417=ORIENTED_EDGE ( 'NONE', *, *, #16501, .F. ) ;
#10422=CARTESIAN_POINT ( 'NONE',  ( -0.3613381517857144343, 0.1758928570453146822, 0.1174058825155740171 ) ) ;
#10426=ORIENTED_EDGE ( 'NONE', *, *, #16501, .T. ) ;
#10429=( BOUNDED_CURVE ( )  B_SPLINE_CURVE ( 2, ( #996, #15994, #10160, #10404, #23172, #19289, #21364, #8423, #21480, #23413, #10514, #17946, #11996 ),
 .UNSPECIFIED., .F., .T. ) 
 B_SPLINE_CURVE_WITH_KNOTS ( ( 3, 2, 2, 2, 2, 2, 3 ),
 ( 0.3928571428571429047, 0.4000000000000000222, 0.4142857142857143127, 0.4285714285714285476, 0.4428571428571428381, 0.4571428571428571286, 0.4642857142857143016 ),
 .UNSPECIFIED. ) 
 CURVE ( )  GEOMETRIC_REPRESENTATION_ITEM ( )  RATIONAL_B_SPLINE_CURVE ( ( 0.9755282581475767101, 0.9755282581475768211, 1.000000000000000000, 0.9510565162951535312, 1.000000000000000000, 0.9510565162951535312, 1.000000000000000000, 0.9510565162951535312, 1.000000000000000000, 0.9510565162951535312, 1.000000000000000000, 0.9755282581475765991, 0.9755282581475767101 ) ) 
 REPRESENTATION_ITEM ( '' )  );
#10468=CARTESIAN_POINT ( 'NONE',  ( 0.2923287055106771337, 0.1437499999024575981, -0.2123892367102620249 ) ) ;
#10495=CARTESIAN_POINT ( 'NONE',  ( 0.000000000000000000, 3.700000000000000622, 0.000000000000000000 ) ) ;
#10497=CARTESIAN_POINT ( 'NONE',  ( 0.1116596296178199027, -0.002678571526113827667, 0.3436530038418508792 ) ) ;
#10499=DIRECTION ( 'NONE',  ( 1.000000000000000000, 0.000000000000000000, 0.000000000000000000 ) ) ;
#10505=ORIENTED_EDGE ( 'NONE', *, *, #14237, .F. ) ;
#10506=CARTESIAN_POINT ( 'NONE',  ( -4.638126268221291196E-16, 0.06071428571428570675, -0.4000000000000000222 ) ) ;
#10511=CARTESIAN_POINT ( 'NONE',  ( 0.1116596296178199860, 0.02589285704531474330, -0.3436530038418508792 ) ) ;
#10514=CARTESIAN_POINT ( 'NONE',  ( 0.1236067977499789861, 0.1910714283763437493, -0.3804226065180614236 ) ) ;
#10520=AXIS2_PLACEMENT_3D ( 'NONE', #19069, #2253, #2377 ) ;
#10533=CARTESIAN_POINT ( 'NONE',  ( -7.726019084026502927E-17, 0.02499999999999997363, 0.4205848896953069405 ) ) ;
#10540=CARTESIAN_POINT ( 'NONE',  ( -4.638126268221291196E-16, 0.1232142855192009251, -0.4000000000000000222 ) ) ;
#10552=ORIENTED_EDGE ( 'NONE', *, *, #2438, .F. ) ;
#10563=CARTESIAN_POINT ( 'NONE',  ( -0.3999999999999999667, 0.3607142857142855430, -0.1299678784931626030 ) ) ;
#10585=CARTESIAN_POINT ( 'NONE',  ( 0.1116596296178199027, 0.4258928570453147100, 0.3436530038418508792 ) ) ;
#10587=CARTESIAN_POINT ( 'NONE',  ( 0.2233192592356399997, 0.2187499999024575814, -0.3073725909049500049 ) ) ;
#10608=EDGE_CURVE ( 'NONE', #15341, #8827, #14773, .T. ) ;
#10612=DIRECTION ( 'NONE',  ( 0.000000000000000000, 0.000000000000000000, -1.000000000000000000 ) ) ;
#10614=CARTESIAN_POINT ( 'NONE',  ( -0.2233192592356399997, 0.1294642856167433076, 0.3073725909049499494 ) ) ;
#10623=CARTESIAN_POINT ( 'NONE',  ( -0.3236067977499790249, 0.08571428571428568732, 0.2351141009169892271 ) ) ;
#10624=EDGE_CURVE ( 'NONE', #10349, #21451, #13067, .T. ) ;
#10628=CARTESIAN_POINT ( 'NONE',  ( 2.326421213736078119E-17, -0.04196428581182809481, -0.3799334167787516425 ) ) ;
#10647=CARTESIAN_POINT ( 'NONE',  ( 0.1116596296178199027, 0.4080357141881718608, 0.3436530038418508792 ) ) ;
#10671=DIRECTION ( 'NONE',  ( 1.000000000000000000, 0.000000000000000000, 0.000000000000000000 ) ) ;
#10679=CARTESIAN_POINT ( 'NONE',  ( -0.2472135954999579999, 0.3749999999999998890, 0.3402603233408160732 ) ) ;
#10692=ORIENTED_EDGE ( 'NONE', *, *, #14352, .F. ) ;
#10696=( BOUNDED_CURVE ( )  B_SPLINE_CURVE ( 2, ( #10506, #16107, #8907, #14277, #17937, #19880, #6961, #16351, #10623, #20124, #18053, #7083, #14522 ),
 .UNSPECIFIED., .F., .F. ) 
 B_SPLINE_CURVE_WITH_KNOTS ( ( 3, 2, 2, 2, 2, 2, 3 ),
 ( 0.3214285714285714524, 0.3285714285714285698, 0.3428571428571428603, 0.3571428571428571508, 0.3714285714285714413, 0.3857142857142857317, 0.3928571428571429047 ),
 .UNSPECIFIED. ) 
 CURVE ( )  GEOMETRIC_REPRESENTATION_ITEM ( )  RATIONAL_B_SPLINE_CURVE ( ( 0.9755282581475767101, 0.9755282581475768211, 1.000000000000000000, 0.9510565162951535312, 1.000000000000000000, 0.9510565162951535312, 1.000000000000000000, 0.9510565162951535312, 1.000000000000000000, 0.9510565162951535312, 1.000000000000000000, 0.9755282581475765991, 0.9755282581475767101 ) ) 
 REPRESENTATION_ITEM ( '' )  );
#10698=CARTESIAN_POINT ( 'NONE',  ( 0.2923287055106771337, 0.3616071427596004306, 0.2123892367102621359 ) ) ;
#10703=CARTESIAN_POINT ( 'NONE',  ( -0.3613381517857143232, 0.3151785713310290005, -4.425116109941954795E-17 ) ) ;
#10736=CARTESIAN_POINT ( 'NONE',  ( 2.326421213736078119E-17, 0.1008928570453146989, -0.3799334167787516425 ) ) ;
#10749=CARTESIAN_POINT ( 'NONE',  ( -0.3613381517857144343, -0.02053571438325666604, 0.1174058825155740171 ) ) ;
#10754=ORIENTED_EDGE ( 'NONE', *, *, #16454, .F. ) ;
#10776=CARTESIAN_POINT ( 'NONE',  ( -0.1236067977499790416, -0.05000000000000000971, 0.3804226065180614236 ) ) ;
#10822=EDGE_CURVE ( 'NONE', #20713, #7372, #19866, .T. ) ;
#10825=CARTESIAN_POINT ( 'NONE',  ( 0.2233192592356399997, 0.3794642856167432798, -0.3073725909049500049 ) ) ;
#10829=CIRCLE ( 'NONE', #13948, 0.03000000000000002318 ) ;
#10857=CARTESIAN_POINT ( 'NONE',  ( 0.2923287055106771337, 0.07589285704531473220, 0.2123892367102621359 ) ) ;
#10860=CARTESIAN_POINT ( 'NONE',  ( 0.3236067977499789694, 0.02678571409062948175, 0.2351141009169893659 ) ) ;
#10870=CARTESIAN_POINT ( 'NONE',  ( 0.3613381517857143232, 0.1544642856167432743, 0.000000000000000000 ) ) ;
#10875=CARTESIAN_POINT ( 'NONE',  ( 0.06335377612981443751, 0.3839733671981016006, 0.4000000000000000222 ) ) ;
#10876=EDGE_CURVE ( 'NONE', #6859, #3037, #15542, .T. ) ;
#10886=DIRECTION ( 'NONE',  ( 0.000000000000000000, 0.000000000000000000, 1.000000000000000000 ) ) ;
#10888=ORIENTED_EDGE ( 'NONE', *, *, #20063, .T. ) ;
#10892=CARTESIAN_POINT ( 'NONE',  ( -0.3236067977499790249, -0.05714285714285716189, 0.2351141009169892271 ) ) ;
#10898=CARTESIAN_POINT ( 'NONE',  ( 2.575339694675500462E-17, 0.05178571409062950742, -0.4205848896953069405 ) ) ;
#10925=CARTESIAN_POINT ( 'NONE',  ( 0.3613381517857143232, 0.2258928570453146989, 0.000000000000000000 ) ) ;
#10979=CARTESIAN_POINT ( 'NONE',  ( -0.2233192592356399442, 0.2508928570453147211, -0.3073725909049500049 ) ) ;
#10992=CARTESIAN_POINT ( 'NONE',  ( -0.2233192592356399997, 0.1294642856167433076, 0.3073725909049499494 ) ) ;
#11011=CARTESIAN_POINT ( 'NONE',  ( 0.4000000000000000222, -0.02857142857142858788, 0.000000000000000000 ) ) ;
#11020=CARTESIAN_POINT ( 'NONE',  ( 0.3999999999999999667, 0.1803571426620581009, -0.1299678784931625475 ) ) ;
#11043=CARTESIAN_POINT ( 'NONE',  ( 0.2233192592356400275, 0.09374999990245759529, -0.3073725909049499494 ) ) ;
#11064=CARTESIAN_POINT ( 'NONE',  ( 0.06335377612981456241, 0.02683051005524446364, 0.3999999999999999667 ) ) ;
#11084=ORIENTED_EDGE ( 'NONE', *, *, #23647, .T. ) ;
#11085=DIRECTION ( 'NONE',  ( 0.000000000000000000, 0.000000000000000000, 1.000000000000000000 ) ) ;
#11093=CARTESIAN_POINT ( 'NONE',  ( 0.1116596296178199860, 0.3116071427596003862, -0.3436530038418508792 ) ) ;
#11101=DIRECTION ( 'NONE',  ( 0.000000000000000000, 0.000000000000000000, 1.000000000000000000 ) ) ;
#11106=CARTESIAN_POINT ( 'NONE',  ( -0.3613381517857143232, 0.2616071427596003973, -4.425116109941954795E-17 ) ) ;
#11113=CARTESIAN_POINT ( 'NONE',  ( 0.3236067977499789694, 0.3928571428571427382, 0.2351141009169893659 ) ) ;
#11123=CARTESIAN_POINT ( 'NONE',  ( 0.000000000000000000, 3.700000000000000622, 0.000000000000000000 ) ) ;
#11131=CARTESIAN_POINT ( 'NONE',  ( 0.3999999999999999667, 0.2535714285714285032, 0.1299678784931626307 ) ) ;
#11138=CARTESIAN_POINT ( 'NONE',  ( 0.2472135954999579721, 0.1160714283763437799, -0.3402603233408159622 ) ) ;
#11145=CARTESIAN_POINT ( 'NONE',  ( -0.3116633497045768197, 3.673292956572201451, -0.09499999999999995948 ) ) ;
#11167=CARTESIAN_POINT ( 'NONE',  ( 0.3613381517857143232, 0.07946428561674330482, 0.1174058825155741975 ) ) ;
#11181=CARTESIAN_POINT ( 'NONE',  ( -0.2923287055106771337, 0.1794642856167432687, 0.2123892367102619971 ) ) ;
#11215=CARTESIAN_POINT ( 'NONE',  ( -0.1116596296178200276, 0.2044642856167432909, 0.3436530038418508792 ) ) ;
#11227=CARTESIAN_POINT ( 'NONE',  ( 0.3613381517857143232, 0.3008928570453147100, -0.1174058825155740587 ) ) ;
#11231=CARTESIAN_POINT ( 'NONE',  ( 0.3311950453211457424, -4.100712535614406822E-18, -0.1463848030125310673 ) ) ;
#11253=CARTESIAN_POINT ( 'NONE',  ( -0.4000000000000000222, 0.1535714285714285254, 0.1299678784931624920 ) ) ;
#11259=CARTESIAN_POINT ( 'NONE',  ( -0.3236067977499789694, 0.1339285712334866152, -0.2351141009169893104 ) ) ;
#11281=CARTESIAN_POINT ( 'NONE',  ( -0.1116596296178200276, -0.02767857152611381821, 0.3436530038418508792 ) ) ;
#11284=CARTESIAN_POINT ( 'NONE',  ( -0.2923287055106771337, 0.1116071427596004445, -0.2123892367102620804 ) ) ;
#11296=DIRECTION ( 'NONE',  ( -1.000000000000000000, -0.000000000000000000, -0.000000000000000000 ) ) ;
#11297=CARTESIAN_POINT ( 'NONE',  ( 0.2923287055106771337, 0.2151785713310289949, -0.2123892367102620249 ) ) ;
#11300=AXIS2_PLACEMENT_3D ( 'NONE', #13578, #4284, #2468 ) ;
#11329=AXIS2_PLACEMENT_3D ( 'NONE', #16462, #3648, #5725 ) ;
#11336=CARTESIAN_POINT ( 'NONE',  ( -0.2233192592356399442, 0.3937499999024575148, -0.3073725909049500049 ) ) ;
#11350=CARTESIAN_POINT ( 'NONE',  ( 0.4749999999999999778, 3.575000000000000622, 0.09499999999999998723 ) ) ;
#11357=ADVANCED_FACE ( 'NONE', ( #2264 ), #14720, .F. ) ;
#11371=CARTESIAN_POINT ( 'NONE',  ( -0.3236067977499790249, 0.1571428571428570564, 0.2351141009169892271 ) ) ;
#11378=CARTESIAN_POINT ( 'NONE',  ( -0.1236067977499789583, 0.05535714266205806616, -0.3804226065180614791 ) ) ;
#11382=FACE_OUTER_BOUND ( 'NONE', #20129, .T. ) ;
#11390=EDGE_CURVE ( 'NONE', #6124, #1426, #12149, .T. ) ;
#11399=CARTESIAN_POINT ( 'NONE',  ( -0.2923287055106771337, 0.02232142847388617762, -0.2123892367102620804 ) ) ;
#11402=CARTESIAN_POINT ( 'NONE',  ( 0.3613381517857143232, 0.1544642856167432743, 0.000000000000000000 ) ) ;
#11419=CARTESIAN_POINT ( 'NONE',  ( 0.3613381517857143232, 0.2116071427596004084, -0.1174058825155740587 ) ) ;
#11440=CARTESIAN_POINT ( 'NONE',  ( -0.1085914856217282259, -6.721771644361021011E-18, 0.3623080614478384476 ) ) ;
#11448=ORIENTED_EDGE ( 'NONE', *, *, #14975, .T. ) ;
#11449=AXIS2_PLACEMENT_3D ( 'NONE', #5603, #22428, #11101 ) ;
#11458=CARTESIAN_POINT ( 'NONE',  ( -0.3613381517857144343, 0.03303571418817188854, 0.1174058825155740171 ) ) ;
#11473=ORIENTED_EDGE ( 'NONE', *, *, #1309, .T. ) ;
#11493=CARTESIAN_POINT ( 'NONE',  ( -0.4000000000000000222, 0.2214285714285713358, -4.898587196589413075E-17 ) ) ;
#11501=CARTESIAN_POINT ( 'NONE',  ( 0.1236067977499789861, 0.4053571426620580787, -0.3804226065180614236 ) ) ;
#11509=CARTESIAN_POINT ( 'NONE',  ( -0.06335377612981497875, 0.2679019384315882712, -0.3999999999999999667 ) ) ;
#11523=CARTESIAN_POINT ( 'NONE',  ( 0.2923287055106771337, 0.0008928570453147542749, -0.2123892367102620249 ) ) ;
#11527=CARTESIAN_POINT ( 'NONE',  ( 0.2923287055106771337, 0.3044642856167432687, -0.2123892367102620249 ) ) ;
#11532=DIRECTION ( 'NONE',  ( 0.000000000000000000, 1.000000000000000000, 0.000000000000000000 ) ) ;
#11542=CARTESIAN_POINT ( 'NONE',  ( -0.3613381517857143788, 0.1758928570453147100, 0.1174058825155740310 ) ) ;
#11551=CARTESIAN_POINT ( 'NONE',  ( -0.3394572874457115752, 3.700000000000000622, -0.09499999999999993172 ) ) ;
#11572=EDGE_CURVE ( 'NONE', #13477, #20558, #20165, .T. ) ;
#11582=CARTESIAN_POINT ( 'NONE',  ( -0.2233192592356399442, 0.01874999990245759460, -0.3073725909049500049 ) ) ;
#11594=DIRECTION ( 'NONE',  ( -1.000000000000000000, 0.000000000000000000, 0.000000000000000000 ) ) ;
#11596=CARTESIAN_POINT ( 'NONE',  ( 0.06335377612981404893, 0.4070980611782420988, -0.4000000000000001887 ) ) ;
#11597=ORIENTED_EDGE ( 'NONE', *, *, #10608, .F. ) ;
#11612=CARTESIAN_POINT ( 'NONE',  ( 2.575339694675500462E-17, 0.2749999999999999112, -0.4205848896953069405 ) ) ;
#11620=CIRCLE ( 'NONE', #21360, 0.4000000000000000222 ) ;
#11621=CARTESIAN_POINT ( 'NONE',  ( -0.4000000000000000222, 0.3589285712334866485, 0.1299678784931624920 ) ) ;
#11624=ADVANCED_FACE ( 'NONE', ( #17856 ), #16023, .T. ) ;
#11639=EDGE_LOOP ( 'NONE', ( #4329, #10108, #4772, #22942 ) ) ;
#11645=CARTESIAN_POINT ( 'NONE',  ( -0.3613381517857143232, 0.02946428561674330898, -4.425116109941954795E-17 ) ) ;
#11649=CARTESIAN_POINT ( 'NONE',  ( 0.3613381517857143232, 0.4401785713310289450, 0.000000000000000000 ) ) ;
#11659=ORIENTED_EDGE ( 'NONE', *, *, #13409, .F. ) ;
#11661=CARTESIAN_POINT ( 'NONE',  ( -0.3613381517857143232, 0.1723214284738861513, -4.425116109941954795E-17 ) ) ;
#11667=FACE_OUTER_BOUND ( 'NONE', #15368, .T. ) ;
#11683=CARTESIAN_POINT ( 'NONE',  ( -0.3875310796859931517, 2.665439728940003759E-18, 0.09388783919108294185 ) ) ;
#11686=CARTESIAN_POINT ( 'NONE',  ( -0.2472135954999579444, 0.2821428571428570287, -0.3402603233408160732 ) ) ;
#11699=CARTESIAN_POINT ( 'NONE',  ( -0.2233192592356399997, -0.03125000009754239083, 0.3073725909049499494 ) ) ;
#11708=CARTESIAN_POINT ( 'NONE',  ( -0.1474902928972388061, -2.846948999568498288E-18, -0.3603575498838690883 ) ) ;
#11712=CARTESIAN_POINT ( 'NONE',  ( 0.000000000000000000, 0.02999999999999995379, 0.3425000000000000266 ) ) ;
#11745=CARTESIAN_POINT ( 'NONE',  ( 0.4000000000000000222, 0.2482142855192009112, 0.000000000000000000 ) ) ;
#11761=ORIENTED_EDGE ( 'NONE', *, *, #23603, .F. ) ;
#11765=CARTESIAN_POINT ( 'NONE',  ( 2.326421213736078119E-17, 0.08303571418817184968, -0.3799334167787516425 ) ) ;
#11768=CARTESIAN_POINT ( 'NONE',  ( -0.2233192592356400275, 0.4151785713310289228, 0.3073725909049499494 ) ) ;
#11769=ORIENTED_EDGE ( 'NONE', *, *, #20202, .F. ) ;
#11778=CARTESIAN_POINT ( 'NONE',  ( -0.3613381517857143232, 0.3116071427596003862, -0.1174058825155741143 ) ) ;
#11782=DIRECTION ( 'NONE',  ( 0.000000000000000000, 0.000000000000000000, 1.000000000000000000 ) ) ;
#11821=CARTESIAN_POINT ( 'NONE',  ( -0.3613381517857143232, 0.02946428561674330898, -4.425116109941954795E-17 ) ) ;
#11846=( BOUNDED_SURFACE ( )  B_SPLINE_SURFACE ( 1, 2, ( 
 ( #24066, #14827, #22243, #12644, #22361, #16999, #9688, #22486, #14940, #3955, #5782, #292, #13244, #7732, #11281, #21015, #3839, #20898, #171, #9446, #4192, #19186, #11523, #16765, #17127, #4069, #15418, #15178, #11399, #13483, #11645, #16880, #22614, #13602, #48, #7967, #6015, #5664, #20544, #18956, #5899, #15298, #2254, #22846, #22725, #11765, #4309, #9566, #20659, #2126, #13128, #18711, #19070, #6135, #13357, #2009, #18831, #416, #7849, #20778, #2378, #9814, #2495, #17247, #531, #7494, #7612, #15064, #4911, #6259, #1138, #10422, #893, #14069, #6382, #8446, #19428, #15534, #17603, #13953, #10298, #23311, #23432, #14184, #8205, #13831, #6618, #21263, #15654, #8324, #4671, #15891, #4553, #6740, #4428, #19791, #21618, #17847, #21496, #9934, #22957, #12373, #17363, #15776, #655, #8573, #4785, #12015, #19547, #21139, #12253, #17722, #8083, #13719, #19668, #1016, #23073, #2726, #11895, #10180, #12140, #19310, #2613, #773, #2839, #6503, #23194, #10057, #17481, #21381, #2966, #16014, #21741, #9052, #18202, #5145, #10647, #12736, #3441, #16617, #22213 ),
 ( #3560, #22095, #24036, #12612, #1618, #12491, #8933, #1257, #20030, #8686, #7231, #3319, #10892, #12975, #10776, #21974, #5391, #3201, #6988, #14307, #11011, #16257, #5513, #20152, #3090, #1498, #16379, #1734, #23790, #18320, #14550, #18079, #5026, #7110, #19912, #10533, #5267, #14430, #16498, #23910, #14676, #12856, #8808, #20273, #18439, #9173, #7346, #14798, #17967, #16134, #1379, #23550, #6864, #23669, #21856, #7703, #15388, #13099, #22816, #18559, #140, #13217, #2093, #17216, #14911, #7583, #7934, #22695, #14, #15150, #4040, #11253, #11371, #22579, #17096, #263, #382, #5867, #7822, #18798, #1849, #20627, #6106, #5633, #18677, #9535, #13326, #15268, #20748, #5986, #11493, #13450, #16968, #9292, #3926, #20392, #20512, #9784, #18928, #11131, #4162, #20868, #15033, #2226, #7462, #11612, #9657, #3684, #16733, #19044, #2346, #1978, #5756, #22331, #500, #3807, #9416, #16853, #22457, #15748, #10149, #8173, #4281, #8538, #20985, #1104, #745, #8058, #19517, #4523, #15627, #21110, #23159, #13923, #2933, #15979, #15506, #19399, #6469, #15861, #11986 ) ),
 .UNSPECIFIED., .F., .F., .F. ) 
 B_SPLINE_SURFACE_WITH_KNOTS ( ( 2, 2 ),
 ( 3, 2, 2, 2, 2, 2, 2, 2, 2, 2, 2, 2, 2, 2, 2, 2, 2, 2, 2, 2, 2, 2, 2, 2, 2, 2, 2, 2, 2, 2, 2, 2, 2, 2, 2, 2, 2, 2, 2, 2, 2, 2, 2, 2, 2, 2, 2, 2, 2, 2, 2, 2, 2, 2, 2, 2, 2, 2, 2, 2, 2, 2, 2, 2, 2, 2, 2, 2, 2, 2, 3 ),
 ( 0.000000000000000000, 1.000000000000000000 ),
 ( 0.000000000000000000, 0.01428571428571428527, 0.02857142857142857054, 0.04285714285714285754, 0.05714285714285714107, 0.07142857142857142461, 0.08571428571428571508, 0.1000000000000000056, 0.1142857142857142821, 0.1285714285714285587, 0.1428571428571428492, 0.1571428571428571397, 0.1714285714285714302, 0.1857142857142857206, 0.2000000000000000111, 0.2142857142857142738, 0.2285714285714285643, 0.2428571428571428548, 0.2571428571428571175, 0.2714285714285714080, 0.2857142857142856984, 0.2999999999999999889, 0.3142857142857142794, 0.3285714285714285698, 0.3428571428571428603, 0.3571428571428571508, 0.3714285714285714413, 0.3857142857142857317, 0.4000000000000000222, 0.4142857142857143127, 0.4285714285714285476, 0.4428571428571428381, 0.4571428571428571286, 0.4714285714285714191, 0.4857142857142857095, 0.5000000000000000000, 0.5142857142857142350, 0.5285714285714285809, 0.5428571428571428159, 0.5571428571428571619, 0.5714285714285713969, 0.5857142857142857428, 0.5999999999999999778, 0.6142857142857143238, 0.6285714285714285587, 0.6428571428571429047, 0.6571428571428571397, 0.6714285714285713746, 0.6857142857142857206, 0.6999999999999999556, 0.7142857142857143016, 0.7285714285714285365, 0.7428571428571428825, 0.7571428571428571175, 0.7714285714285714635, 0.7857142857142856984, 0.8000000000000000444, 0.8142857142857142794, 0.8285714285714286254, 0.8428571428571428603, 0.8571428571428570953, 0.8714285714285714413, 0.8857142857142856762, 0.9000000000000000222, 0.9142857142857142572, 0.9285714285714286031, 0.9428571428571428381, 0.9571428571428571841, 0.9714285714285714191, 0.9857142857142857650, 1.000000000000000000 ),
 .UNSPECIFIED. ) 
 GEOMETRIC_REPRESENTATION_ITEM ( )  RATIONAL_B_SPLINE_SURFACE ( (
 ( 1.000000000000000000, 0.9510565162951535312, 1.000000000000000000, 0.9510565162951535312, 1.000000000000000000, 0.9510565162951535312, 1.000000000000000000, 0.9510565162951535312, 1.000000000000000000, 0.9510565162951535312, 1.000000000000000000, 0.9510565162951535312, 1.000000000000000000, 0.9510565162951535312, 1.000000000000000000, 0.9510565162951535312, 1.000000000000000000, 0.9510565162951535312, 1.000000000000000000, 0.9510565162951535312, 1.000000000000000000, 0.9510565162951535312, 1.000000000000000000, 0.9510565162951535312, 1.000000000000000000, 0.9510565162951535312, 1.000000000000000000, 0.9510565162951535312, 1.000000000000000000, 0.9510565162951535312, 1.000000000000000000, 0.9510565162951535312, 1.000000000000000000, 0.9510565162951535312, 1.000000000000000000, 0.9510565162951535312, 1.000000000000000000, 0.9510565162951535312, 1.000000000000000000, 0.9510565162951535312, 1.000000000000000000, 0.9510565162951535312, 1.000000000000000000, 0.9510565162951535312, 1.000000000000000000, 0.9510565162951535312, 1.000000000000000000, 0.9510565162951535312, 1.000000000000000000, 0.9510565162951535312, 1.000000000000000000, 0.9510565162951535312, 1.000000000000000000, 0.9510565162951535312, 1.000000000000000000, 0.9510565162951535312, 1.000000000000000000, 0.9510565162951535312, 1.000000000000000000, 0.9510565162951535312, 1.000000000000000000, 0.9510565162951535312, 1.000000000000000000, 0.9510565162951535312, 1.000000000000000000, 0.9510565162951535312, 1.000000000000000000, 0.9510565162951535312, 1.000000000000000000, 0.9510565162951535312, 1.000000000000000000, 0.9510565162951535312, 1.000000000000000000, 0.9510565162951535312, 1.000000000000000000, 0.9510565162951535312, 1.000000000000000000, 0.9510565162951535312, 1.000000000000000000, 0.9510565162951535312, 1.000000000000000000, 0.9510565162951535312, 1.000000000000000000, 0.9510565162951535312, 1.000000000000000000, 0.9510565162951535312, 1.000000000000000000, 0.9510565162951535312, 1.000000000000000000, 0.9510565162951535312, 1.000000000000000000, 0.9510565162951535312, 1.000000000000000000, 0.9510565162951535312, 1.000000000000000000, 0.9510565162951535312, 1.000000000000000000, 0.9510565162951535312, 1.000000000000000000, 0.9510565162951535312, 1.000000000000000000, 0.9510565162951535312, 1.000000000000000000, 0.9510565162951535312, 1.000000000000000000, 0.9510565162951535312, 1.000000000000000000, 0.9510565162951535312, 1.000000000000000000, 0.9510565162951535312, 1.000000000000000000, 0.9510565162951535312, 1.000000000000000000, 0.9510565162951535312, 1.000000000000000000, 0.9510565162951535312, 1.000000000000000000, 0.9510565162951535312, 1.000000000000000000, 0.9510565162951535312, 1.000000000000000000, 0.9510565162951535312, 1.000000000000000000, 0.9510565162951535312, 1.000000000000000000, 0.9510565162951535312, 1.000000000000000000, 0.9510565162951535312, 1.000000000000000000, 0.9510565162951535312, 1.000000000000000000, 0.9510565162951535312, 1.000000000000000000, 0.9510565162951535312, 1.000000000000000000, 0.9510565162951535312, 1.000000000000000000, 0.9510565162951535312, 1.000000000000000000, 0.9510565162951535312, 1.000000000000000000),
 ( 1.000000000000000000, 0.9510565162951535312, 1.000000000000000000, 0.9510565162951535312, 1.000000000000000000, 0.9510565162951535312, 1.000000000000000000, 0.9510565162951535312, 1.000000000000000000, 0.9510565162951535312, 1.000000000000000000, 0.9510565162951535312, 1.000000000000000000, 0.9510565162951535312, 1.000000000000000000, 0.9510565162951535312, 1.000000000000000000, 0.9510565162951535312, 1.000000000000000000, 0.9510565162951535312, 1.000000000000000000, 0.9510565162951535312, 1.000000000000000000, 0.9510565162951535312, 1.000000000000000000, 0.9510565162951535312, 1.000000000000000000, 0.9510565162951535312, 1.000000000000000000, 0.9510565162951535312, 1.000000000000000000, 0.9510565162951535312, 1.000000000000000000, 0.9510565162951535312, 1.000000000000000000, 0.9510565162951535312, 1.000000000000000000, 0.9510565162951535312, 1.000000000000000000, 0.9510565162951535312, 1.000000000000000000, 0.9510565162951535312, 1.000000000000000000, 0.9510565162951535312, 1.000000000000000000, 0.9510565162951535312, 1.000000000000000000, 0.9510565162951535312, 1.000000000000000000, 0.9510565162951535312, 1.000000000000000000, 0.9510565162951535312, 1.000000000000000000, 0.9510565162951535312, 1.000000000000000000, 0.9510565162951535312, 1.000000000000000000, 0.9510565162951535312, 1.000000000000000000, 0.9510565162951535312, 1.000000000000000000, 0.9510565162951535312, 1.000000000000000000, 0.9510565162951535312, 1.000000000000000000, 0.9510565162951535312, 1.000000000000000000, 0.9510565162951535312, 1.000000000000000000, 0.9510565162951535312, 1.000000000000000000, 0.9510565162951535312, 1.000000000000000000, 0.9510565162951535312, 1.000000000000000000, 0.9510565162951535312, 1.000000000000000000, 0.9510565162951535312, 1.000000000000000000, 0.9510565162951535312, 1.000000000000000000, 0.9510565162951535312, 1.000000000000000000, 0.9510565162951535312, 1.000000000000000000, 0.9510565162951535312, 1.000000000000000000, 0.9510565162951535312, 1.000000000000000000, 0.9510565162951535312, 1.000000000000000000, 0.9510565162951535312, 1.000000000000000000, 0.9510565162951535312, 1.000000000000000000, 0.9510565162951535312, 1.000000000000000000, 0.9510565162951535312, 1.000000000000000000, 0.9510565162951535312, 1.000000000000000000, 0.9510565162951535312, 1.000000000000000000, 0.9510565162951535312, 1.000000000000000000, 0.9510565162951535312, 1.000000000000000000, 0.9510565162951535312, 1.000000000000000000, 0.9510565162951535312, 1.000000000000000000, 0.9510565162951535312, 1.000000000000000000, 0.9510565162951535312, 1.000000000000000000, 0.9510565162951535312, 1.000000000000000000, 0.9510565162951535312, 1.000000000000000000, 0.9510565162951535312, 1.000000000000000000, 0.9510565162951535312, 1.000000000000000000, 0.9510565162951535312, 1.000000000000000000, 0.9510565162951535312, 1.000000000000000000, 0.9510565162951535312, 1.000000000000000000, 0.9510565162951535312, 1.000000000000000000, 0.9510565162951535312, 1.000000000000000000, 0.9510565162951535312, 1.000000000000000000, 0.9510565162951535312, 1.000000000000000000, 0.9510565162951535312, 1.000000000000000000, 0.9510565162951535312, 1.000000000000000000) ) ) 
 REPRESENTATION_ITEM ( '' )  SURFACE ( )  );
#11857=ORIENTED_EDGE ( 'NONE', *, *, #6925, .T. ) ;
#11872=CARTESIAN_POINT ( 'NONE',  ( 0.1236067977499789861, 0.2624999998049151739, -0.3804226065180614236 ) ) ;
#11882=ORIENTED_EDGE ( 'NONE', *, *, #13467, .F. ) ;
#11890=ORIENTED_EDGE ( 'NONE', *, *, #4978, .T. ) ;
#11895=CARTESIAN_POINT ( 'NONE',  ( 0.2923287055106771337, 0.3437499999024575814, 0.2123892367102621359 ) ) ;
#11898=CARTESIAN_POINT ( 'NONE',  ( 0.3613381517857143232, 0.3651785713310288783, 0.1174058825155741975 ) ) ;
#11918=LINE ( 'NONE', #19570, #22027 ) ;
#11920=CARTESIAN_POINT ( 'NONE',  ( -4.638126268221291196E-16, 0.1946428569477723358, -0.4000000000000000222 ) ) ;
#11924=ORIENTED_EDGE ( 'NONE', *, *, #23996, .T. ) ;
#11930=CARTESIAN_POINT ( 'NONE',  ( 0.07641315408907055351, -6.434570819605719236E-16, 0.3613612515901026834 ) ) ;
#11950=CARTESIAN_POINT ( 'NONE',  ( -0.3613381517857143232, 0.09732142847388615403, -0.1174058825155741004 ) ) ;
#11981=CARTESIAN_POINT ( 'NONE',  ( 0.2977100099089716734, 3.659999999999999698, 0.09499999999999995948 ) ) ;
#11986=CARTESIAN_POINT ( 'NONE',  ( 0.4000000000000000222, 0.3999999999999999112, 0.000000000000000000 ) ) ;
#11994=CARTESIAN_POINT ( 'NONE',  ( 0.1236067977499789028, 0.3053571426620580453, 0.3804226065180614791 ) ) ;
#11996=CARTESIAN_POINT ( 'NONE',  ( -4.638126268221291196E-16, 0.1946428569477723358, -0.4000000000000000222 ) ) ;
#12007=CARTESIAN_POINT ( 'NONE',  ( 0.2472135954999579721, 0.3392857142857141350, -0.3402603233408160732 ) ) ;
#12013=CARTESIAN_POINT ( 'NONE',  ( -0.06335377612981447915, 0.02316948994475548362, 0.4000000000000000777 ) ) ;
#12015=CARTESIAN_POINT ( 'NONE',  ( -0.2233192592356399442, 0.3044642856167432132, -0.3073725909049500049 ) ) ;
#12018=CARTESIAN_POINT ( 'NONE',  ( 0.3613381517857143232, 0.3687499999024574926, 0.000000000000000000 ) ) ;
#12019=CARTESIAN_POINT ( 'NONE',  ( -0.4000000000000000222, 0.1410714283763437604, -4.898587196589413075E-17 ) ) ;
#12030=CARTESIAN_POINT ( 'NONE',  ( 0.3613381517857143232, 0.2758928570453146878, 0.1174058825155741975 ) ) ;
#12040=CYLINDRICAL_SURFACE ( 'NONE', #6965, 0.4000000000000000222 ) ;
#12067=CARTESIAN_POINT ( 'NONE',  ( -0.2233192592356399442, 0.3044642856167432132, -0.3073725909049500049 ) ) ;
#12102=CARTESIAN_POINT ( 'NONE',  ( 0.3999999999999999667, 0.2535714285714285032, 0.1299678784931626307 ) ) ;
#12115=CARTESIAN_POINT ( 'NONE',  ( -0.2923287055106771337, 0.1258928570453147489, 0.2123892367102619971 ) ) ;
#12118=CYLINDRICAL_SURFACE ( 'NONE', #12391, 0.4000000000000000222 ) ;
#12140=CARTESIAN_POINT ( 'NONE',  ( 0.3613381517857143232, 0.3508928570453146989, 0.000000000000000000 ) ) ;
#12149=LINE ( 'NONE', #7859, #3128 ) ;
#12153=ORIENTED_EDGE ( 'NONE', *, *, #16212, .T. ) ;
#12168=DIRECTION ( 'NONE',  ( -0.000000000000000000, -1.000000000000000000, -0.000000000000000000 ) ) ;
#12191=CARTESIAN_POINT ( 'NONE',  ( -6.979263641208234666E-17, 0.3330357141881717942, 0.3799334167787516425 ) ) ;
#12206=CARTESIAN_POINT ( 'NONE',  ( 0.3615179832709032870, -1.207678508861138611E-18, 0.002776101469111443704 ) ) ;
#12219=CARTESIAN_POINT ( 'NONE',  ( 0.2923287055106771337, 0.1473214284738861568, 0.2123892367102621359 ) ) ;
#12224=DIRECTION ( 'NONE',  ( 0.000000000000000000, 1.000000000000000000, 0.000000000000000000 ) ) ;
#12229=CARTESIAN_POINT ( 'NONE',  ( -9.626299801968715084E-16, 0.2035714285714284866, -0.4000000000000000222 ) ) ;
#12232=CARTESIAN_POINT ( 'NONE',  ( -6.979263641208234666E-17, 0.06517857133102902822, 0.3799334167787516425 ) ) ;
#12252=DIRECTION ( 'NONE',  ( -0.000000000000000000, -1.000000000000000000, -0.000000000000000000 ) ) ;
#12253=CARTESIAN_POINT ( 'NONE',  ( -0.3613381517857143232, 0.3151785713310290005, -4.425116109941954795E-17 ) ) ;
#12301=CARTESIAN_POINT ( 'NONE',  ( 0.3613381517857143232, 0.3723214284738861068, -0.1174058825155740587 ) ) ;
#12302=EDGE_CURVE ( 'NONE', #5943, #15879, #10415, .T. ) ;
#12304=CARTESIAN_POINT ( 'NONE',  ( -0.2923287055106771337, 0.2366071427596004584, -0.2123892367102620804 ) ) ;
#12326=CARTESIAN_POINT ( 'NONE',  ( -0.3613381517857143232, 0.02589285704531474330, -0.1174058825155741143 ) ) ;
#12338=CARTESIAN_POINT ( 'NONE',  ( 0.3613381517857143232, -0.05625000009754239222, -0.1174058825155740587 ) ) ;
#12342=LINE ( 'NONE', #861, #1444 ) ;
#12350=CARTESIAN_POINT ( 'NONE',  ( -0.1116596296178199582, -0.03839285724039952913, -0.3436530038418508792 ) ) ;
#12354=DIRECTION ( 'NONE',  ( -0.000000000000000000, -1.000000000000000000, -0.000000000000000000 ) ) ;
#12373=CARTESIAN_POINT ( 'NONE',  ( 0.3613381517857143232, 0.2830357141881717498, -0.1174058825155740587 ) ) ;
#12391=AXIS2_PLACEMENT_3D ( 'NONE', #8916, #23528, #14285 ) ;
#12401=CARTESIAN_POINT ( 'NONE',  ( -9.626299801968715084E-16, 0.3464285714285713635, -0.4000000000000000222 ) ) ;
#12409=CARTESIAN_POINT ( 'NONE',  ( 0.4749999999999999778, 3.575000000000000622, 2.908536147974959276E-17 ) ) ;
#12421=( BOUNDED_CURVE ( )  B_SPLINE_CURVE ( 2, ( #12401, #8714, #8837, #14335, #1165, #10563, #3352, #16286, #1409, #10679, #18234, #21767, #8964 ),
 .UNSPECIFIED., .F., .F. ) 
 B_SPLINE_CURVE_WITH_KNOTS ( ( 3, 2, 2, 2, 2, 2, 3 ),
 ( 0.8928571428571429047, 0.9000000000000000222, 0.9142857142857142572, 0.9285714285714286031, 0.9428571428571428381, 0.9571428571428571841, 0.9642857142857143016 ),
 .UNSPECIFIED. ) 
 CURVE ( )  GEOMETRIC_REPRESENTATION_ITEM ( )  RATIONAL_B_SPLINE_CURVE ( ( 0.9755282581475768211, 0.9755282581475769321, 1.000000000000000000, 0.9510565162951535312, 1.000000000000000000, 0.9510565162951535312, 1.000000000000000000, 0.9510565162951535312, 1.000000000000000000, 0.9510565162951535312, 1.000000000000000000, 0.9755282581475768211, 0.9755282581475768211 ) ) 
 REPRESENTATION_ITEM ( '' )  );
#12425=CARTESIAN_POINT ( 'NONE',  ( -0.2233192592356399997, 0.2544642856167432243, 0.3073725909049499494 ) ) ;
#12428=CARTESIAN_POINT ( 'NONE',  ( 0.3613381517857143232, 0.2294642856167432854, -0.1174058825155740587 ) ) ;
#12444=CARTESIAN_POINT ( 'NONE',  ( 0.2977100099089716734, 3.659999999999999698, -0.09499999999999995948 ) ) ;
#12453=CARTESIAN_POINT ( 'NONE',  ( 0.3613381517857143232, 0.008035714188171885417, 0.1174058825155742114 ) ) ;
#12464=CARTESIAN_POINT ( 'NONE',  ( -0.2233192592356399997, 0.05803571418817188299, 0.3073725909049499494 ) ) ;
#12476=VECTOR ( 'NONE', #11296, 39.37007874015748143 ) ;
#12479=CARTESIAN_POINT ( 'NONE',  ( 0.06335377612981404893, 0.2642409183210992496, -0.4000000000000001887 ) ) ;
#12491=CARTESIAN_POINT ( 'NONE',  ( 2.575339694675500462E-17, -0.08214285714285715634, -0.4205848896953069405 ) ) ;
#12524=ORIENTED_EDGE ( 'NONE', *, *, #20063, .F. ) ;
#12534=AXIS2_PLACEMENT_3D ( 'NONE', #10495, #17925, #10612 ) ;
#12536=ORIENTED_EDGE ( 'NONE', *, *, #4662, .T. ) ;
#12545=CARTESIAN_POINT ( 'NONE',  ( -0.2923287055106771337, 0.3080357141881718275, -0.2123892367102620804 ) ) ;
#12552=CARTESIAN_POINT ( 'NONE',  ( 0.3999999999999999667, 0.1107142857142856956, 0.1299678784931626307 ) ) ;
#12573=CARTESIAN_POINT ( 'NONE',  ( -6.979263641208234666E-17, 0.06517857133102901435, 0.3799334167787516425 ) ) ;
#12583=CARTESIAN_POINT ( 'NONE',  ( 4.898587196589413075E-17, 3.700000000000000622, 0.4000000000000000222 ) ) ;
#12586=CARTESIAN_POINT ( 'NONE',  ( 0.2923287055106771337, 0.09017857133102902267, -0.2123892367102620249 ) ) ;
#12608=VERTEX_POINT ( 'NONE', #976 ) ;
#12612=CARTESIAN_POINT ( 'NONE',  ( 0.2472135954999579721, -0.08928571428571427382, -0.3402603233408159622 ) ) ;
#12618=PLANE ( 'NONE',  #10107 ) ;
#12620=ADVANCED_FACE ( 'NONE', ( #15973 ), #8529, .T. ) ;
#12626=CARTESIAN_POINT ( 'NONE',  ( -0.3236067977499789694, 0.2053571426620580398, -0.2351141009169893104 ) ) ;
#12644=CARTESIAN_POINT ( 'NONE',  ( 0.2233192592356399997, -0.06696428581182808926, -0.3073725909049500049 ) ) ;
#12667=CARTESIAN_POINT ( 'NONE',  ( 0.2923287055106771337, 0.3437499999024575814, 0.2123892367102621359 ) ) ;
#12670=ADVANCED_FACE ( 'NONE', ( #6463 ), #1338, .F. ) ;
#12673=AXIS2_PLACEMENT_3D ( 'NONE', #18856, #4089, #11782 ) ;
#12701=CARTESIAN_POINT ( 'NONE',  ( 0.3613381517857143232, 0.08303571418817186356, 0.000000000000000000 ) ) ;
#12704=CARTESIAN_POINT ( 'NONE',  ( 0.3806690758928571450, 0.4111607142369430590, 0.000000000000000000 ) ) ;
#12708=ORIENTED_EDGE ( 'NONE', *, *, #19200, .F. ) ;
#12714=CARTESIAN_POINT ( 'NONE',  ( -0.3613381517857144343, 0.1937499999024576147, 0.1174058825155740171 ) ) ;
#12736=CARTESIAN_POINT ( 'NONE',  ( 0.2233192592356399164, 0.4116071427596004750, 0.3073725909049500604 ) ) ;
#12738=( BOUNDED_CURVE ( )  B_SPLINE_CURVE ( 2, ( #22202, #3429, #14785, #7099, #18547, #14537, #1837, #16722, #21960, #2, #5013, #12479, #19898 ),
 .UNSPECIFIED., .F., .T. ) 
 B_SPLINE_CURVE_WITH_KNOTS ( ( 3, 2, 2, 2, 2, 2, 3 ),
 ( 0.5357142857142856984, 0.5428571428571428159, 0.5571428571428571619, 0.5714285714285713969, 0.5857142857142857428, 0.5999999999999999778, 0.6071428571428572063 ),
 .UNSPECIFIED. ) 
 CURVE ( )  GEOMETRIC_REPRESENTATION_ITEM ( )  RATIONAL_B_SPLINE_CURVE ( ( 0.9755282581475768211, 0.9755282581475768211, 1.000000000000000000, 0.9510565162951535312, 1.000000000000000000, 0.9510565162951535312, 1.000000000000000000, 0.9510565162951535312, 1.000000000000000000, 0.9510565162951535312, 1.000000000000000000, 0.9755282581475765991, 0.9755282581475768211 ) ) 
 REPRESENTATION_ITEM ( '' )  );
#12744=FACE_OUTER_BOUND ( 'NONE', #19330, .T. ) ;
#12750=AXIS2_PLACEMENT_3D ( 'NONE', #19874, #8411, #23044 ) ;
#12789=CARTESIAN_POINT ( 'NONE',  ( 1.750236327630675537E-16, 0.02499999999999997710, 0.3999999999999999667 ) ) ;
#12790=CARTESIAN_POINT ( 'NONE',  ( -0.2923287055106771337, 0.3794642856167432798, -0.2123892367102620804 ) ) ;
#12820=CARTESIAN_POINT ( 'NONE',  ( 0.2923287055106771337, 0.2330357141881718441, -0.2123892367102620249 ) ) ;
#12833=CARTESIAN_POINT ( 'NONE',  ( -0.1116596296178199582, 0.3187499999024575592, -0.3436530038418508792 ) ) ;
#12836=DIRECTION ( 'NONE',  ( 0.000000000000000000, 0.000000000000000000, 1.000000000000000000 ) ) ;
#12838=EDGE_LOOP ( 'NONE', ( #24088, #5055, #2506, #3621 ) ) ;
#12856=CARTESIAN_POINT ( 'NONE',  ( 0.3999999999999999667, 0.04642857142857139546, -0.1299678784931625475 ) ) ;
#12862=CARTESIAN_POINT ( 'NONE',  ( 0.3999999999999999667, 0.1017857140906294894, 0.1299678784931626307 ) ) ;
#12869=CIRCLE ( 'NONE', #13624, 0.03000000000000002318 ) ;
#12877=EDGE_LOOP ( 'NONE', ( #20024, #11448, #14065, #3027 ) ) ;
#12892=CARTESIAN_POINT ( 'NONE',  ( -0.3613381517857143788, 0.1223214284738861485, 0.1174058825155740310 ) ) ;
#12902=EDGE_CURVE ( 'NONE', #20713, #13860, #3644, .T. ) ;
#12906=FACE_OUTER_BOUND ( 'NONE', #9411, .T. ) ;
#12912=CARTESIAN_POINT ( 'NONE',  ( 0.3613381517857143232, 0.4187499999024575370, 0.1174058825155742114 ) ) ;
#12916=EDGE_LOOP ( 'NONE', ( #23691, #20057, #20026, #2208, #3220, #15317, #3102, #16729 ) ) ;
#12931=( BOUNDED_CURVE ( )  B_SPLINE_CURVE ( 2, ( #10540, #17973, #6264, #779, #6385, #13834, #12019, #19432, #17606, #897, #16389, #16506, #1858 ),
 .UNSPECIFIED., .F., .F. ) 
 B_SPLINE_CURVE_WITH_KNOTS ( ( 3, 2, 2, 2, 2, 2, 3 ),
 ( 0.3214285714285714524, 0.3285714285714285698, 0.3428571428571428603, 0.3571428571428571508, 0.3714285714285714413, 0.3857142857142857317, 0.3928571428571429047 ),
 .UNSPECIFIED. ) 
 CURVE ( )  GEOMETRIC_REPRESENTATION_ITEM ( )  RATIONAL_B_SPLINE_CURVE ( ( 0.9755282581475767101, 0.9755282581475768211, 1.000000000000000000, 0.9510565162951535312, 1.000000000000000000, 0.9510565162951535312, 1.000000000000000000, 0.9510565162951535312, 1.000000000000000000, 0.9510565162951535312, 1.000000000000000000, 0.9755282581475765991, 0.9755282581475767101 ) ) 
 REPRESENTATION_ITEM ( '' )  );
#12944=CARTESIAN_POINT ( 'NONE',  ( 0.2233192592356399164, 0.2151785713310289672, 0.3073725909049500604 ) ) ;
#12956=CARTESIAN_POINT ( 'NONE',  ( -0.2233192592356399442, 0.2508928570453147211, -0.3073725909049500049 ) ) ;
#12958=DIRECTION ( 'NONE',  ( -0.000000000000000000, 1.000000000000000000, -0.000000000000000000 ) ) ;
#12973=CARTESIAN_POINT ( 'NONE',  ( -0.4749999999999999778, 3.700000000000000622, 2.908536147974962357E-17 ) ) ;
#12975=CARTESIAN_POINT ( 'NONE',  ( -0.2472135954999579999, -0.05357142857142858927, 0.3402603233408159622 ) ) ;
#12984=CARTESIAN_POINT ( 'NONE',  ( -7.726019084026502927E-17, 0.08749999980491522666, 0.4205848896953069405 ) ) ;
#12991=CARTESIAN_POINT ( 'NONE',  ( -0.2977100099089716734, 3.659999999999999698, -0.09499999999999995948 ) ) ;
#12995=ORIENTED_EDGE ( 'NONE', *, *, #5116, .F. ) ;
#13009=CARTESIAN_POINT ( 'NONE',  ( 0.2233192592356400275, 0.1651785713310290615, -0.3073725909049499494 ) ) ;
#13010=ORIENTED_EDGE ( 'NONE', *, *, #18562, .F. ) ;
#13023=CARTESIAN_POINT ( 'NONE',  ( 0.1116596296178199860, 0.2223214284738861402, -0.3436530038418508792 ) ) ;
#13033=CARTESIAN_POINT ( 'NONE',  ( 0.3613381517857143232, 0.3508928570453146989, 0.000000000000000000 ) ) ;
#13039=CARTESIAN_POINT ( 'NONE',  ( -0.3236067977499790249, 0.07678571409062948105, 0.2351141009169892271 ) ) ;
#13059=CARTESIAN_POINT ( 'NONE',  ( -0.3613381517857143232, 0.2616071427596003973, -4.425116109941954795E-17 ) ) ;
#13067=( BOUNDED_CURVE ( )  B_SPLINE_CURVE ( 2, ( #15031, #22578, #20511, #6105, #13097, #5985, #9415, #18676, #19043, #4280, #20747, #1848, #18926 ),
 .UNSPECIFIED., .F., .F. ) 
 B_SPLINE_CURVE_WITH_KNOTS ( ( 3, 2, 2, 2, 2, 2, 3 ),
 ( 0.7500000000000000000, 0.7571428571428571175, 0.7714285714285714635, 0.7857142857142856984, 0.8000000000000000444, 0.8142857142857142794, 0.8214285714285715079 ),
 .UNSPECIFIED. ) 
 CURVE ( )  GEOMETRIC_REPRESENTATION_ITEM ( )  RATIONAL_B_SPLINE_CURVE ( ( 0.9755282581475768211, 0.9755282581475768211, 1.000000000000000000, 0.9510565162951535312, 1.000000000000000000, 0.9510565162951535312, 1.000000000000000000, 0.9510565162951535312, 1.000000000000000000, 0.9510565162951535312, 1.000000000000000000, 0.9755282581475765991, 0.9755282581475768211 ) ) 
 REPRESENTATION_ITEM ( '' )  );
#13072=CARTESIAN_POINT ( 'NONE',  ( 0.1116596296178199027, 0.2830357141881718053, 0.3436530038418508792 ) ) ;
#13097=CARTESIAN_POINT ( 'NONE',  ( -0.3236067977499789694, 0.3482142855192008613, -0.2351141009169893104 ) ) ;
#13099=CARTESIAN_POINT ( 'NONE',  ( 0.2472135954999579166, 0.1035714285714285227, 0.3402603233408160732 ) ) ;
#13106=CARTESIAN_POINT ( 'NONE',  ( 0.3999999999999999667, 0.1089285712334866069, -0.1299678784931625475 ) ) ;
#13117=VERTEX_POINT ( 'NONE', #22484 ) ;
#13128=CARTESIAN_POINT ( 'NONE',  ( -0.3613381517857143232, 0.1008928570453147405, -4.425116109941954795E-17 ) ) ;
#13131=CARTESIAN_POINT ( 'NONE',  ( -0.2233192592356399442, 0.1080357141881718996, -0.3073725909049499494 ) ) ;
#13144=CARTESIAN_POINT ( 'NONE',  ( 0.2923287055106771337, 0.05803571418817188299, 0.2123892367102621359 ) ) ;
#13155=DIRECTION ( 'NONE',  ( -1.000000000000000000, -0.000000000000000000, -0.000000000000000000 ) ) ;
#13162=CARTESIAN_POINT ( 'NONE',  ( -0.1236067977499789583, 0.05535714266205805228, -0.3804226065180614791 ) ) ;
#13182=CARTESIAN_POINT ( 'NONE',  ( -0.1116596296178199582, 0.3187499999024575592, -0.3436530038418508792 ) ) ;
#13196=VERTEX_POINT ( 'NONE', #1882 ) ;
#13212=ORIENTED_EDGE ( 'NONE', *, *, #2764, .F. ) ;
#13217=CARTESIAN_POINT ( 'NONE',  ( 0.3999999999999999667, 0.1178571428571428270, -0.1299678784931625475 ) ) ;
#13224=CARTESIAN_POINT ( 'NONE',  ( 0.2472135954999579721, 0.04464285694777236219, -0.3402603233408159622 ) ) ;
#13231=CARTESIAN_POINT ( 'NONE',  ( -0.3236067977499790249, 0.2910714283763437549, 0.2351141009169892271 ) ) ;
#13244=CARTESIAN_POINT ( 'NONE',  ( -0.2923287055106771337, -0.03482142866897096345, 0.2123892367102619971 ) ) ;
#13247=CARTESIAN_POINT ( 'NONE',  ( 0.3613381517857143232, 0.1580357141881718608, -0.1174058825155740587 ) ) ;
#13256=ADVANCED_FACE ( 'NONE', ( #1642 ), #7729, .F. ) ;
#13262=CARTESIAN_POINT ( 'NONE',  ( 0.3613381517857143232, 0.06160714275960043479, 0.1174058825155741975 ) ) ;
#13263=VERTEX_POINT ( 'NONE', #22358 ) ;
#13271=ORIENTED_EDGE ( 'NONE', *, *, #7063, .F. ) ;
#13278=CARTESIAN_POINT ( 'NONE',  ( 1.750236327630675537E-16, 0.08749999980491518503, 0.3999999999999999667 ) ) ;
#13279=VECTOR ( 'NONE', #4757, 39.37007874015748143 ) ;
#13299=CARTESIAN_POINT ( 'NONE',  ( -0.2923287055106771337, 0.1973214284738861179, 0.2123892367102619971 ) ) ;
#13313=CARTESIAN_POINT ( 'NONE',  ( 0.1236067977499789861, 0.3339285712334865708, -0.3804226065180614236 ) ) ;
#13326=CARTESIAN_POINT ( 'NONE',  ( -0.1236067977499789583, 0.2071428571428570731, -0.3804226065180614791 ) ) ;
#13333=ORIENTED_EDGE ( 'NONE', *, *, #7522, .F. ) ;
#13335=CARTESIAN_POINT ( 'NONE',  ( 0.2472135954999579721, 0.1874999998049151628, -0.3402603233408159622 ) ) ;
#13343=EDGE_CURVE ( 'NONE', #15982, #22290, #7610, .T. ) ;
#13347=AXIS2_PLACEMENT_3D ( 'NONE', #3625, #1920, #20219 ) ;
#13357=CARTESIAN_POINT ( 'NONE',  ( -0.1116596296178200276, 0.1151785713310290032, 0.3436530038418508792 ) ) ;
#13358=DIRECTION ( 'NONE',  ( 0.000000000000000000, 1.000000000000000000, 0.000000000000000000 ) ) ;
#13361=CARTESIAN_POINT ( 'NONE',  ( -0.2923287055106771337, 0.3258928570453146767, -0.2123892367102620804 ) ) ;
#13375=CARTESIAN_POINT ( 'NONE',  ( -0.2923287055106771337, 0.09374999990245758141, -0.2123892367102620804 ) ) ;
#13409=EDGE_CURVE ( 'NONE', #20523, #22475, #437, .T. ) ;
#13411=CARTESIAN_POINT ( 'NONE',  ( -0.1116596296178199582, 0.08660714275960045005, -0.3436530038418508792 ) ) ;
#13414=CARTESIAN_POINT ( 'NONE',  ( 9.184850993605150903E-17, 2.735000000000000320, -0.7500000000000001110 ) ) ;
#13431=CARTESIAN_POINT ( 'NONE',  ( 9.101228903679513089E-16, 0.3017857140906293756, 0.4000000000000000222 ) ) ;
#13434=CARTESIAN_POINT ( 'NONE',  ( 0.000000000000000000, 0.02999999999999995379, 0.000000000000000000 ) ) ;
#13450=CARTESIAN_POINT ( 'NONE',  ( -0.4000000000000000222, 0.2249999999999999500, 0.1299678784931624920 ) ) ;
#13458=CARTESIAN_POINT ( 'NONE',  ( -0.3236067977499789694, 0.2053571426620580676, -0.2351141009169893104 ) ) ;
#13467=EDGE_CURVE ( 'NONE', #6124, #7372, #15295, .T. ) ;
#13477=VERTEX_POINT ( 'NONE', #19067 ) ;
#13480=CARTESIAN_POINT ( 'NONE',  ( -0.3236067977499789694, -1.707404996040164512E-17, -0.2351141009169893104 ) ) ;
#13483=CARTESIAN_POINT ( 'NONE',  ( -0.3613381517857143232, 0.02589285704531474330, -0.1174058825155741004 ) ) ;
#13485=ORIENTED_EDGE ( 'NONE', *, *, #19811, .F. ) ;
#13487=CARTESIAN_POINT ( 'NONE',  ( -0.3613381517857143232, 0.2616071427596003973, -4.425116109941954795E-17 ) ) ;
#13500=CARTESIAN_POINT ( 'NONE',  ( 0.3613381517857143232, 0.1401785713310289838, -0.1174058825155740587 ) ) ;
#13518=CARTESIAN_POINT ( 'NONE',  ( -0.06335377612981497875, 0.4107590812887310094, -0.3999999999999999667 ) ) ;
#13523=CARTESIAN_POINT ( 'NONE',  ( -0.04734746964375153438, 4.708926481085645203E-18, 0.3720189177726724306 ) ) ;
#13538=ORIENTED_EDGE ( 'NONE', *, *, #19811, .T. ) ;
#13539=CARTESIAN_POINT ( 'NONE',  ( -0.3613381517857143232, 0.4008928570453146878, -0.1174058825155741004 ) ) ;
#13558=CARTESIAN_POINT ( 'NONE',  ( 1.750236327630675475E-17, 0.3374999998049151295, -0.3999999999999999667 ) ) ;
#13563=TOROIDAL_SURFACE ( 'NONE', #8867, 0.3425000000000000266, 0.02999999999999999889 ) ;
#13575=CARTESIAN_POINT ( 'NONE',  ( -0.3798103452830965954, 0.002729592702593379612, 0.1577565542260639386 ) ) ;
#13578=CARTESIAN_POINT ( 'NONE',  ( -0.4749999999999999778, 3.575000000000000622, -0.09499999999999995948 ) ) ;
#13583=CARTESIAN_POINT ( 'NONE',  ( -0.3236067977499790249, 0.2196428569477723303, 0.2351141009169892271 ) ) ;
#13601=FACE_OUTER_BOUND ( 'NONE', #12877, .T. ) ;
#13602=CARTESIAN_POINT ( 'NONE',  ( -0.2233192592356399997, 0.04017857133102901990, 0.3073725909049499494 ) ) ;
#13605=CARTESIAN_POINT ( 'NONE',  ( 0.3613381517857143232, 0.3008928570453147100, -0.1174058825155740587 ) ) ;
#13617=CARTESIAN_POINT ( 'NONE',  ( 0.2233192592356400275, 0.2901785713310290338, -0.3073725909049499494 ) ) ;
#13621=CARTESIAN_POINT ( 'NONE',  ( 0.3255746763033851021, 3.686631053841027850, -0.09499999999999995948 ) ) ;
#13622=DIRECTION ( 'NONE',  ( 0.000000000000000000, 0.000000000000000000, -1.000000000000000000 ) ) ;
#13624=AXIS2_PLACEMENT_3D ( 'NONE', #1210, #6814, #14257 ) ;
#13657=CARTESIAN_POINT ( 'NONE',  ( 0.3613381517857143232, -0.07410714295468522061, -0.1174058825155740587 ) ) ;
#13661=CARTESIAN_POINT ( 'NONE',  ( 0.2472135954999579721, 0.04464285694777234831, -0.3402603233408160732 ) ) ;
#13667=CARTESIAN_POINT ( 'NONE',  ( 0.06335377612981456241, 0.08933050986015969586, 0.3999999999999999667 ) ) ;
#13668=CARTESIAN_POINT ( 'NONE',  ( 0.2320196243301847205, 1.046010598739759003E-17, -0.2860823100163923383 ) ) ;
#13674=CARTESIAN_POINT ( 'NONE',  ( 0.3601051986570594221, -1.207678508861135529E-18, 0.03795131042432794977 ) ) ;
#13679=CARTESIAN_POINT ( 'NONE',  ( 0.3613381517857143232, 0.3544642856167432576, -0.1174058825155740587 ) ) ;
#13682=AXIS2_PLACEMENT_3D ( 'NONE', #1774, #22257, #13960 ) ;
#13691=CARTESIAN_POINT ( 'NONE',  ( -0.4000000000000000222, 0.1535714285714285254, 0.1299678784931624920 ) ) ;
#13701=CARTESIAN_POINT ( 'NONE',  ( 0.3236067977499789694, 0.3839285712334866152, 0.2351141009169893659 ) ) ;
#13711=CARTESIAN_POINT ( 'NONE',  ( 0.3236067977499790249, 0.3357142857142856318, -0.2351141009169892826 ) ) ;
#13716=CARTESIAN_POINT ( 'NONE',  ( -0.2472135954999579999, 0.01785714285714282493, 0.3402603233408160732 ) ) ;
#13719=CARTESIAN_POINT ( 'NONE',  ( -0.2233192592356399997, 0.3258928570453145657, 0.3073725909049499494 ) ) ;
#13722=CARTESIAN_POINT ( 'NONE',  ( 2.326421213736078119E-17, 0.3151785713310290005, -0.3799334167787516980 ) ) ;
#13725=DIRECTION ( 'NONE',  ( 0.000000000000000000, 0.000000000000000000, 1.000000000000000000 ) ) ;
#13731=CARTESIAN_POINT ( 'NONE',  ( -0.2233192592356400275, 0.2544642856167432798, 0.3073725909049499494 ) ) ;
#13733=VERTEX_POINT ( 'NONE', #19573 ) ;
#13741=DIRECTION ( 'NONE',  ( 0.000000000000000000, 0.000000000000000000, -1.000000000000000000 ) ) ;
#13762=ADVANCED_FACE ( 'NONE', ( #15685, #14097 ), #4814, .F. ) ;
#13766=CARTESIAN_POINT ( 'NONE',  ( 0.1116596296178199860, 0.07946428561674331870, -0.3436530038418508792 ) ) ;
#13769=CARTESIAN_POINT ( 'NONE',  ( 0.2923287055106771337, 0.004464285616743319737, 0.2123892367102621359 ) ) ;
#13771=CARTESIAN_POINT ( 'NONE',  ( 9.001153973733040933E-17, 3.700000000000000622, 0.7199999999999994182 ) ) ;
#13772=EDGE_LOOP ( 'NONE', ( #7319, #22946, #1289, #2509 ) ) ;
#13781=CARTESIAN_POINT ( 'NONE',  ( 0.3178873086046067331, 2.458266394542412200E-17, 0.1722007902088446563 ) ) ;
#13782=ORIENTED_EDGE ( 'NONE', *, *, #11390, .T. ) ;
#13785=EDGE_CURVE ( 'NONE', #21724, #13860, #7412, .T. ) ;
#13799=CARTESIAN_POINT ( 'NONE',  ( 0.4000000000000000222, 0.4624999998049150740, 0.000000000000000000 ) ) ;
#13807=CARTESIAN_POINT ( 'NONE',  ( 0.3236067977499790249, 0.3982142855192009057, -0.2351141009169892826 ) ) ;
#13831=CARTESIAN_POINT ( 'NONE',  ( 2.326421213736078119E-17, 0.2258928570453146711, -0.3799334167787516425 ) ) ;
#13833=CARTESIAN_POINT ( 'NONE',  ( -0.1116596296178199582, 0.2473214284738861346, -0.3436530038418508792 ) ) ;
#13834=CARTESIAN_POINT ( 'NONE',  ( -0.3999999999999999667, 0.1374999998049151739, -0.1299678784931626030 ) ) ;
#13838=( BOUNDED_SURFACE ( )  B_SPLINE_SURFACE ( 1, 2, ( 
 ( #20159, #17397, #1740, #1857, #22338, #7590, #14919, #15042, #5641, #22464, #9300, #9058, #3691, #20757, #22221, #5764, #7470, #2101, #18568, #9181, #5520, #16624, #22102, #13224, #18685, #10898, #11378, #18328, #16975, #16862, #23, #14684, #1624, #20519, #20634, #12984, #3566, #3936, #23918, #12862, #24044, #13106, #20400, #11138, #14804, #3817, #147, #16741, #11259, #18444, #1987, #9423, #271, #5874, #18806, #5397, #9542, #20281, #7711, #15157, #22589, #11020, #7353, #13335, #16505, #7237, #15396, #508, #13458, #20876, #752, #4170, #13583, #10037, #15635, #20993, #9909, #17459, #15515, #2353, #11745, #4531, #8180, #2591, #11872, #19408, #22939, #10156, #634, #4288, #22823, #870, #18936, #17341, #2705, #17581, #11994, #23167, #19166, #21118, #9794, #2233, #6114, #17227, #2474, #7941, #8065, #22703, #8303, #15275, #23052, #11621, #19052, #6360, #6479, #6235, #4047, #4408, #13701, #15755, #13930, #19285, #13807, #21243, #11501, #9666, #17103, #391, #7830, #5993, #10274, #1237, #17699, #23409, #14162, #3178, #23285, #4885, #991, #2941, #15868 ),
 ( #8662, #8546, #15988, #1114, #14281, #10628, #12350, #6717, #4760, #6841, #21719, #10749, #16355, #19767, #8420, #19525, #6598, #3064, #21830, #16236, #18181, #21592, #19886, #14046, #10511, #2818, #17941, #21477, #1353, #16111, #5003, #7087, #23524, #12464, #23646, #12232, #18057, #8784, #6966, #14406, #5121, #19642, #12586, #10399, #17822, #20009, #3295, #1474, #8912, #23766, #21361, #4648, #12115, #10992, #7204, #3659, #18536, #9394, #7559, #24015, #10870, #5242, #18299, #16593, #20487, #22309, #16834, #18417, #9271, #9032, #7325, #12714, #1711, #20128, #7443, #9150, #1826, #22432, #14777, #20368, #5607, #23886, #20251, #22191, #5490, #14527, #1597, #12956, #23593, #14650, #11106, #15012, #117, #16712, #14890, #5367, #13072, #3539, #3420, #16475, #3783, #11227, #18656, #1948, #21949, #22071, #12833, #23600, #1432, #14232, #19962, #18134, #7041, #23716, #4833, #1187, #23478, #3374, #10698, #6915, #7161, #12301, #14602, #10825, #5194, #3133, #2885, #8985, #6669, #6793, #23839, #14480, #15935, #14354, #3250, #3018, #10585, #21786, #8859, #16188, #16303 ) ),
 .UNSPECIFIED., .F., .F., .F. ) 
 B_SPLINE_SURFACE_WITH_KNOTS ( ( 2, 2 ),
 ( 3, 2, 2, 2, 2, 2, 2, 2, 2, 2, 2, 2, 2, 2, 2, 2, 2, 2, 2, 2, 2, 2, 2, 2, 2, 2, 2, 2, 2, 2, 2, 2, 2, 2, 2, 2, 2, 2, 2, 2, 2, 2, 2, 2, 2, 2, 2, 2, 2, 2, 2, 2, 2, 2, 2, 2, 2, 2, 2, 2, 2, 2, 2, 2, 2, 2, 2, 2, 2, 2, 3 ),
 ( 0.000000000000000000, 1.000000000000000000 ),
 ( 0.000000000000000000, 0.01428571428571428527, 0.02857142857142857054, 0.04285714285714285754, 0.05714285714285714107, 0.07142857142857142461, 0.08571428571428571508, 0.1000000000000000056, 0.1142857142857142821, 0.1285714285714285587, 0.1428571428571428492, 0.1571428571428571397, 0.1714285714285714302, 0.1857142857142857206, 0.2000000000000000111, 0.2142857142857142738, 0.2285714285714285643, 0.2428571428571428548, 0.2571428571428571175, 0.2714285714285714080, 0.2857142857142856984, 0.2999999999999999889, 0.3142857142857142794, 0.3285714285714285698, 0.3428571428571428603, 0.3571428571428571508, 0.3714285714285714413, 0.3857142857142857317, 0.4000000000000000222, 0.4142857142857143127, 0.4285714285714285476, 0.4428571428571428381, 0.4571428571428571286, 0.4714285714285714191, 0.4857142857142857095, 0.5000000000000000000, 0.5142857142857142350, 0.5285714285714285809, 0.5428571428571428159, 0.5571428571428571619, 0.5714285714285713969, 0.5857142857142857428, 0.5999999999999999778, 0.6142857142857143238, 0.6285714285714285587, 0.6428571428571429047, 0.6571428571428571397, 0.6714285714285713746, 0.6857142857142857206, 0.6999999999999999556, 0.7142857142857143016, 0.7285714285714285365, 0.7428571428571428825, 0.7571428571428571175, 0.7714285714285714635, 0.7857142857142856984, 0.8000000000000000444, 0.8142857142857142794, 0.8285714285714286254, 0.8428571428571428603, 0.8571428571428570953, 0.8714285714285714413, 0.8857142857142856762, 0.9000000000000000222, 0.9142857142857142572, 0.9285714285714286031, 0.9428571428571428381, 0.9571428571428571841, 0.9714285714285714191, 0.9857142857142857650, 1.000000000000000000 ),
 .UNSPECIFIED. ) 
 GEOMETRIC_REPRESENTATION_ITEM ( )  RATIONAL_B_SPLINE_SURFACE ( (
 ( 1.000000000000000000, 0.9510565162951535312, 1.000000000000000000, 0.9510565162951535312, 1.000000000000000000, 0.9510565162951535312, 1.000000000000000000, 0.9510565162951535312, 1.000000000000000000, 0.9510565162951535312, 1.000000000000000000, 0.9510565162951535312, 1.000000000000000000, 0.9510565162951535312, 1.000000000000000000, 0.9510565162951535312, 1.000000000000000000, 0.9510565162951535312, 1.000000000000000000, 0.9510565162951535312, 1.000000000000000000, 0.9510565162951535312, 1.000000000000000000, 0.9510565162951535312, 1.000000000000000000, 0.9510565162951535312, 1.000000000000000000, 0.9510565162951535312, 1.000000000000000000, 0.9510565162951535312, 1.000000000000000000, 0.9510565162951535312, 1.000000000000000000, 0.9510565162951535312, 1.000000000000000000, 0.9510565162951535312, 1.000000000000000000, 0.9510565162951535312, 1.000000000000000000, 0.9510565162951535312, 1.000000000000000000, 0.9510565162951535312, 1.000000000000000000, 0.9510565162951535312, 1.000000000000000000, 0.9510565162951535312, 1.000000000000000000, 0.9510565162951535312, 1.000000000000000000, 0.9510565162951535312, 1.000000000000000000, 0.9510565162951535312, 1.000000000000000000, 0.9510565162951535312, 1.000000000000000000, 0.9510565162951535312, 1.000000000000000000, 0.9510565162951535312, 1.000000000000000000, 0.9510565162951535312, 1.000000000000000000, 0.9510565162951535312, 1.000000000000000000, 0.9510565162951535312, 1.000000000000000000, 0.9510565162951535312, 1.000000000000000000, 0.9510565162951535312, 1.000000000000000000, 0.9510565162951535312, 1.000000000000000000, 0.9510565162951535312, 1.000000000000000000, 0.9510565162951535312, 1.000000000000000000, 0.9510565162951535312, 1.000000000000000000, 0.9510565162951535312, 1.000000000000000000, 0.9510565162951535312, 1.000000000000000000, 0.9510565162951535312, 1.000000000000000000, 0.9510565162951535312, 1.000000000000000000, 0.9510565162951535312, 1.000000000000000000, 0.9510565162951535312, 1.000000000000000000, 0.9510565162951535312, 1.000000000000000000, 0.9510565162951535312, 1.000000000000000000, 0.9510565162951535312, 1.000000000000000000, 0.9510565162951535312, 1.000000000000000000, 0.9510565162951535312, 1.000000000000000000, 0.9510565162951535312, 1.000000000000000000, 0.9510565162951535312, 1.000000000000000000, 0.9510565162951535312, 1.000000000000000000, 0.9510565162951535312, 1.000000000000000000, 0.9510565162951535312, 1.000000000000000000, 0.9510565162951535312, 1.000000000000000000, 0.9510565162951535312, 1.000000000000000000, 0.9510565162951535312, 1.000000000000000000, 0.9510565162951535312, 1.000000000000000000, 0.9510565162951535312, 1.000000000000000000, 0.9510565162951535312, 1.000000000000000000, 0.9510565162951535312, 1.000000000000000000, 0.9510565162951535312, 1.000000000000000000, 0.9510565162951535312, 1.000000000000000000, 0.9510565162951535312, 1.000000000000000000, 0.9510565162951535312, 1.000000000000000000, 0.9510565162951535312, 1.000000000000000000, 0.9510565162951535312, 1.000000000000000000, 0.9510565162951535312, 1.000000000000000000, 0.9510565162951535312, 1.000000000000000000, 0.9510565162951535312, 1.000000000000000000),
 ( 1.000000000000000000, 0.9510565162951535312, 1.000000000000000000, 0.9510565162951535312, 1.000000000000000000, 0.9510565162951535312, 1.000000000000000000, 0.9510565162951535312, 1.000000000000000000, 0.9510565162951535312, 1.000000000000000000, 0.9510565162951535312, 1.000000000000000000, 0.9510565162951535312, 1.000000000000000000, 0.9510565162951535312, 1.000000000000000000, 0.9510565162951535312, 1.000000000000000000, 0.9510565162951535312, 1.000000000000000000, 0.9510565162951535312, 1.000000000000000000, 0.9510565162951535312, 1.000000000000000000, 0.9510565162951535312, 1.000000000000000000, 0.9510565162951535312, 1.000000000000000000, 0.9510565162951535312, 1.000000000000000000, 0.9510565162951535312, 1.000000000000000000, 0.9510565162951535312, 1.000000000000000000, 0.9510565162951535312, 1.000000000000000000, 0.9510565162951535312, 1.000000000000000000, 0.9510565162951535312, 1.000000000000000000, 0.9510565162951535312, 1.000000000000000000, 0.9510565162951535312, 1.000000000000000000, 0.9510565162951535312, 1.000000000000000000, 0.9510565162951535312, 1.000000000000000000, 0.9510565162951535312, 1.000000000000000000, 0.9510565162951535312, 1.000000000000000000, 0.9510565162951535312, 1.000000000000000000, 0.9510565162951535312, 1.000000000000000000, 0.9510565162951535312, 1.000000000000000000, 0.9510565162951535312, 1.000000000000000000, 0.9510565162951535312, 1.000000000000000000, 0.9510565162951535312, 1.000000000000000000, 0.9510565162951535312, 1.000000000000000000, 0.9510565162951535312, 1.000000000000000000, 0.9510565162951535312, 1.000000000000000000, 0.9510565162951535312, 1.000000000000000000, 0.9510565162951535312, 1.000000000000000000, 0.9510565162951535312, 1.000000000000000000, 0.9510565162951535312, 1.000000000000000000, 0.9510565162951535312, 1.000000000000000000, 0.9510565162951535312, 1.000000000000000000, 0.9510565162951535312, 1.000000000000000000, 0.9510565162951535312, 1.000000000000000000, 0.9510565162951535312, 1.000000000000000000, 0.9510565162951535312, 1.000000000000000000, 0.9510565162951535312, 1.000000000000000000, 0.9510565162951535312, 1.000000000000000000, 0.9510565162951535312, 1.000000000000000000, 0.9510565162951535312, 1.000000000000000000, 0.9510565162951535312, 1.000000000000000000, 0.9510565162951535312, 1.000000000000000000, 0.9510565162951535312, 1.000000000000000000, 0.9510565162951535312, 1.000000000000000000, 0.9510565162951535312, 1.000000000000000000, 0.9510565162951535312, 1.000000000000000000, 0.9510565162951535312, 1.000000000000000000, 0.9510565162951535312, 1.000000000000000000, 0.9510565162951535312, 1.000000000000000000, 0.9510565162951535312, 1.000000000000000000, 0.9510565162951535312, 1.000000000000000000, 0.9510565162951535312, 1.000000000000000000, 0.9510565162951535312, 1.000000000000000000, 0.9510565162951535312, 1.000000000000000000, 0.9510565162951535312, 1.000000000000000000, 0.9510565162951535312, 1.000000000000000000, 0.9510565162951535312, 1.000000000000000000, 0.9510565162951535312, 1.000000000000000000, 0.9510565162951535312, 1.000000000000000000, 0.9510565162951535312, 1.000000000000000000, 0.9510565162951535312, 1.000000000000000000) ) ) 
 REPRESENTATION_ITEM ( '' )  SURFACE ( )  );
#13847=CARTESIAN_POINT ( 'NONE',  ( 0.3613381517857143232, 0.2830357141881718053, -0.1174058825155740587 ) ) ;
#13860=VERTEX_POINT ( 'NONE', #17696 ) ;
#13864=ORIENTED_EDGE ( 'NONE', *, *, #13409, .T. ) ;
#13865=CYLINDRICAL_SURFACE ( 'NONE', #7758, 0.4000000000000000222 ) ;
#13887=CARTESIAN_POINT ( 'NONE',  ( -0.3613381517857143232, 0.02589285704531474330, -0.1174058825155741004 ) ) ;
#13908=CARTESIAN_POINT ( 'NONE',  ( -0.2923287055106771337, 0.3937499999024575148, 0.2123892367102619971 ) ) ;
#13923=CARTESIAN_POINT ( 'NONE',  ( -0.2472135954999579999, 0.3749999999999999445, 0.3402603233408159622 ) ) ;
#13930=CARTESIAN_POINT ( 'NONE',  ( 0.4000000000000000222, 0.3910714283763437327, 0.000000000000000000 ) ) ;
#13948=AXIS2_PLACEMENT_3D ( 'NONE', #11712, #11594, #2675 ) ;
#13953=CARTESIAN_POINT ( 'NONE',  ( 0.3613381517857143232, 0.2044642856167432632, 0.1174058825155742114 ) ) ;
#13960=DIRECTION ( 'NONE',  ( -1.000000000000000000, 0.000000000000000000, -0.000000000000000000 ) ) ;
#13969=VERTEX_POINT ( 'NONE', #12229 ) ;
#13984=EDGE_CURVE ( 'NONE', #13733, #20678, #15865, .T. ) ;
#13991=CARTESIAN_POINT ( 'NONE',  ( 0.000000000000000000, 2.735000000000000320, 0.000000000000000000 ) ) ;
#13999=DIRECTION ( 'NONE',  ( 0.000000000000000000, 1.000000000000000000, 0.000000000000000000 ) ) ;
#14000=CARTESIAN_POINT ( 'NONE',  ( -0.1116596296178199582, 0.3008928570453147100, -0.3436530038418508792 ) ) ;
#14007=EDGE_CURVE ( 'NONE', #17359, #7539, #19087, .T. ) ;
#14024=CARTESIAN_POINT ( 'NONE',  ( 2.326421213736078119E-17, 0.01160714275960046671, -0.3799334167787516980 ) ) ;
#14034=CARTESIAN_POINT ( 'NONE',  ( 0.2233192592356399164, 0.1437499999024575703, 0.3073725909049500604 ) ) ;
#14046=CARTESIAN_POINT ( 'NONE',  ( 0.2233192592356399997, 0.02232142847388618109, -0.3073725909049500049 ) ) ;
#14065=ORIENTED_EDGE ( 'NONE', *, *, #21743, .T. ) ;
#14069=CARTESIAN_POINT ( 'NONE',  ( -0.2233192592356399997, 0.1830357141881718830, 0.3073725909049499494 ) ) ;
#14076=CARTESIAN_POINT ( 'NONE',  ( -0.4000000000000000222, 0.2160714283763437438, 0.1299678784931624920 ) ) ;
#14097=FACE_BOUND ( 'NONE', #2497, .T. ) ;
#14118=CARTESIAN_POINT ( 'NONE',  ( 0.2233192592356399164, 0.1258928570453146933, 0.3073725909049500604 ) ) ;
#14126=CARTESIAN_POINT ( 'NONE',  ( 4.113055369932088708E-16, 0.09642857142857140518, 0.4000000000000000222 ) ) ;
#14132=LINE ( 'NONE', #4853, #6130 ) ;
#14137=AXIS2_PLACEMENT_3D ( 'NONE', #8480, #19703, #8357 ) ;
#14146=DIRECTION ( 'NONE',  ( 0.000000000000000000, 0.000000000000000000, 1.000000000000000000 ) ) ;
#14148=CARTESIAN_POINT ( 'NONE',  ( 0.2233192592356399164, 0.07232142847388617346, 0.3073725909049500604 ) ) ;
#14162=CARTESIAN_POINT ( 'NONE',  ( -0.1236067977499790416, 0.4410714283763437216, 0.3804226065180614236 ) ) ;
#14184=CARTESIAN_POINT ( 'NONE',  ( 0.2233192592356399997, 0.2187499999024575814, -0.3073725909049500049 ) ) ;
#14193=DIRECTION ( 'NONE',  ( 0.000000000000000000, 0.000000000000000000, 1.000000000000000000 ) ) ;
#14196=CARTESIAN_POINT ( 'NONE',  ( -0.06335377612981457629, 0.2285266326068134957, 0.3999999999999999667 ) ) ;
#14232=CARTESIAN_POINT ( 'NONE',  ( -0.3613381517857143232, 0.3294642856167431799, -0.1174058825155741004 ) ) ;
#14236=CARTESIAN_POINT ( 'NONE',  ( 0.2923287055106771337, 0.2723214284738861291, 0.2123892367102621359 ) ) ;
#14237=EDGE_CURVE ( 'NONE', #23116, #13196, #15541, .T. ) ;
#14247=DIRECTION ( 'NONE',  ( 0.000000000000000000, 1.000000000000000000, 0.000000000000000000 ) ) ;
#14257=DIRECTION ( 'NONE',  ( 1.224646799147352221E-16, 0.000000000000000000, -1.000000000000000000 ) ) ;
#14268=CARTESIAN_POINT ( 'NONE',  ( -0.2233192592356399442, 0.1080357141881718719, -0.3073725909049500049 ) ) ;
#14277=CARTESIAN_POINT ( 'NONE',  ( -0.2472135954999579444, 0.06785714285714283811, -0.3402603233408160732 ) ) ;
#14281=CARTESIAN_POINT ( 'NONE',  ( 0.1116596296178199860, -0.04553571438325666743, -0.3436530038418508792 ) ) ;
#14285=DIRECTION ( 'NONE',  ( 0.000000000000000000, 0.000000000000000000, -1.000000000000000000 ) ) ;
#14286=( BOUNDED_CURVE ( )  B_SPLINE_CURVE ( 2, ( #5230, #21820, #3285, #18169, #10860, #18289, #1465, #9022, #8024, #13661, #17059, #22424, #16827 ),
 .UNSPECIFIED., .F., .F. ) 
 B_SPLINE_CURVE_WITH_KNOTS ( ( 3, 2, 2, 2, 2, 2, 3 ),
 ( 0.1071428571428571508, 0.1142857142857142821, 0.1285714285714285587, 0.1428571428571428492, 0.1571428571428571397, 0.1714285714285714302, 0.1785714285714285754 ),
 .UNSPECIFIED. ) 
 CURVE ( )  GEOMETRIC_REPRESENTATION_ITEM ( )  RATIONAL_B_SPLINE_CURVE ( ( 0.9755282581475768211, 0.9755282581475768211, 1.000000000000000000, 0.9510565162951535312, 1.000000000000000000, 0.9510565162951535312, 1.000000000000000000, 0.9510565162951535312, 1.000000000000000000, 0.9510565162951535312, 1.000000000000000000, 0.9755282581475768211, 0.9755282581475768211 ) ) 
 REPRESENTATION_ITEM ( '' )  );
#14299=DIRECTION ( 'NONE',  ( -0.000000000000000000, -1.000000000000000000, -0.000000000000000000 ) ) ;
#14307=CARTESIAN_POINT ( 'NONE',  ( 0.3999999999999999667, -0.03214285714285715356, 0.1299678784931626307 ) ) ;
#14335=CARTESIAN_POINT ( 'NONE',  ( -0.2472135954999579444, 0.3535714285714284810, -0.3402603233408160732 ) ) ;
#14352=EDGE_CURVE ( 'NONE', #2478, #5171, #2356, .T. ) ;
#14354=CARTESIAN_POINT ( 'NONE',  ( -0.2233192592356399997, 0.4151785713310289783, 0.3073725909049499494 ) ) ;
#14358=CARTESIAN_POINT ( 'NONE',  ( -0.3613381517857143232, 0.2437499999024575481, -4.425116109941954795E-17 ) ) ;
#14365=CARTESIAN_POINT ( 'NONE',  ( 0.000000000000000000, 3.659999999999999698, 0.000000000000000000 ) ) ;
#14378=ADVANCED_FACE ( 'NONE', ( #21797 ), #2742, .F. ) ;
#14379=EDGE_CURVE ( 'NONE', #15066, #6859, #20527, .T. ) ;
#14391=CARTESIAN_POINT ( 'NONE',  ( 0.3613381517857143232, 0.01517857133102902024, -0.1174058825155740587 ) ) ;
#14406=CARTESIAN_POINT ( 'NONE',  ( 0.3613381517857143232, 0.07946428561674330482, 0.1174058825155742114 ) ) ;
#14410=FACE_OUTER_BOUND ( 'NONE', #3313, .T. ) ;
#14430=CARTESIAN_POINT ( 'NONE',  ( 0.2472135954999579166, 0.03214285714285712581, 0.3402603233408160732 ) ) ;
#14435=CARTESIAN_POINT ( 'NONE',  ( 0.000000000000000000, 2.735000000000000320, 0.000000000000000000 ) ) ;
#14438=CARTESIAN_POINT ( 'NONE',  ( 0.000000000000000000, 3.700000000000000622, 0.000000000000000000 ) ) ;
#14445=CARTESIAN_POINT ( 'NONE',  ( -0.1236067977499789583, 0.1982142855192008668, -0.3804226065180614791 ) ) ;
#14480=CARTESIAN_POINT ( 'NONE',  ( -0.3613381517857144343, 0.4080357141881717498, 0.1174058825155740171 ) ) ;
#14482=CARTESIAN_POINT ( 'NONE',  ( 0.1116596296178199027, 0.1937499999024575870, 0.3436530038418508792 ) ) ;
#14505=VECTOR ( 'NONE', #6904, 39.37007874015748143 ) ;
#14513=CARTESIAN_POINT ( 'NONE',  ( -0.2233192592356399442, -0.03482142866897096345, -0.3073725909049500049 ) ) ;
#14522=CARTESIAN_POINT ( 'NONE',  ( 4.113055369932088708E-16, 0.09642857142857140518, 0.4000000000000000222 ) ) ;
#14527=CARTESIAN_POINT ( 'NONE',  ( 2.326421213736078119E-17, 0.2437499999024574926, -0.3799334167787516425 ) ) ;
#14530=CARTESIAN_POINT ( 'NONE',  ( 0.000000000000000000, 0.02999999999999995379, 0.000000000000000000 ) ) ;
#14533=CARTESIAN_POINT ( 'NONE',  ( 0.2472135954999579166, 0.3892857142857142350, 0.3402603233408160732 ) ) ;
#14537=CARTESIAN_POINT ( 'NONE',  ( 0.3999999999999999667, 0.2446428569477722970, 0.1299678784931626307 ) ) ;
#14542=EDGE_CURVE ( 'NONE', #13117, #16849, #86, .T. ) ;
#14544=EDGE_LOOP ( 'NONE', ( #6289, #8734, #23519, #19100, #9951 ) ) ;
#14550=CARTESIAN_POINT ( 'NONE',  ( -0.4000000000000000222, 0.007142857142857113144, -4.898587196589413075E-17 ) ) ;
#14602=CARTESIAN_POINT ( 'NONE',  ( 0.2923287055106771337, 0.3758928570453146656, -0.2123892367102620249 ) ) ;
#14613=CARTESIAN_POINT ( 'NONE',  ( -0.4000000000000000222, 0.06964285694777233582, -4.898587196589413075E-17 ) ) ;
#14637=CARTESIAN_POINT ( 'NONE',  ( 0.1116596296178199027, 0.3544642856167432576, 0.3436530038418508792 ) ) ;
#14640=DIRECTION ( 'NONE',  ( -0.8660254037844394848, 0.4999999999999983902, -0.000000000000000000 ) ) ;
#14650=CARTESIAN_POINT ( 'NONE',  ( -0.3613381517857143232, 0.2580357141881718386, -0.1174058825155741004 ) ) ;
#14663=VECTOR ( 'NONE', #20028, 39.37007874015748143 ) ;
#14676=CARTESIAN_POINT ( 'NONE',  ( 0.4000000000000000222, 0.04285714285714282978, 0.000000000000000000 ) ) ;
#14684=CARTESIAN_POINT ( 'NONE',  ( -0.4000000000000000222, 0.07321428551920092231, 0.1299678784931624920 ) ) ;
#14690=VECTOR ( 'NONE', #22783, 39.37007874015748143 ) ;
#14712=CARTESIAN_POINT ( 'NONE',  ( -0.1116596296178200276, 0.06160714275960046254, 0.3436530038418508792 ) ) ;
#14720=PLANE ( 'NONE',  #13682 ) ;
#14723=EDGE_CURVE ( 'NONE', #20411, #2118, #7905, .T. ) ;
#14725=CARTESIAN_POINT ( 'NONE',  ( -0.2977100099089716734, 3.659999999999999698, 0.09499999999999995948 ) ) ;
#14734=CARTESIAN_POINT ( 'NONE',  ( 0.1116596296178199860, 0.3651785713310289894, -0.3436530038418508792 ) ) ;
#14752=ORIENTED_EDGE ( 'NONE', *, *, #20202, .T. ) ;
#14755=CARTESIAN_POINT ( 'NONE',  ( 0.000000000000000000, 2.735000000000000320, 0.000000000000000000 ) ) ;
#14762=CARTESIAN_POINT ( 'NONE',  ( -0.4749999999999999778, 3.700000000000000622, -0.09499999999999995948 ) ) ;
#14763=CARTESIAN_POINT ( 'NONE',  ( 0.3613381517857143232, 0.2258928570453146989, 0.000000000000000000 ) ) ;
#14773=( BOUNDED_CURVE ( )  B_SPLINE_CURVE ( 2, ( #262, #13575, #16852, #15149, #4161, #5632, #499 ),
 .UNSPECIFIED., .F., .F. ) 
 B_SPLINE_CURVE_WITH_KNOTS ( ( 3, 2, 2, 3 ),
 ( 0.07506635404883826856, 0.08571428571428571508, 0.1000000000000000056, 0.1071428571428571508 ),
 .UNSPECIFIED. ) 
 CURVE ( )  GEOMETRIC_REPRESENTATION_ITEM ( )  RATIONAL_B_SPLINE_CURVE ( ( 0.9814209735438260696, 0.9635197191029298835, 1.000000000000000000, 0.9510565162951535312, 1.000000000000000000, 0.9755282581475768211, 0.9755282581475768211 ) ) 
 REPRESENTATION_ITEM ( '' )  );
#14777=CARTESIAN_POINT ( 'NONE',  ( 0.2923287055106771337, 0.2187499999024575537, 0.2123892367102621359 ) ) ;
#14785=CARTESIAN_POINT ( 'NONE',  ( 0.1236067977499789028, 0.2339285712334865930, 0.3804226065180614791 ) ) ;
#14798=CARTESIAN_POINT ( 'NONE',  ( -0.2472135954999579444, 0.06785714285714283811, -0.3402603233408159622 ) ) ;
#14804=CARTESIAN_POINT ( 'NONE',  ( 0.1236067977499789861, 0.1196428569477723663, -0.3804226065180614236 ) ) ;
#14815=EDGE_CURVE ( 'NONE', #13733, #769, #18813, .T. ) ;
#14827=CARTESIAN_POINT ( 'NONE',  ( 0.3613381517857143232, -0.07410714295468522061, -0.1174058825155740587 ) ) ;
#14831=CARTESIAN_POINT ( 'NONE',  ( 0.2233192592356399164, 0.07232142847388617346, 0.3073725909049500604 ) ) ;
#14838=CARTESIAN_POINT ( 'NONE',  ( 9.184850993605150903E-17, 3.669999999999999929, -0.7500000000000001110 ) ) ;
#14847=CARTESIAN_POINT ( 'NONE',  ( 0.3084175934503982641, -2.427762526784286478E-18, -0.1882653658700420007 ) ) ;
#14863=EDGE_CURVE ( 'NONE', #20713, #17619, #8651, .T. ) ;
#14880=CARTESIAN_POINT ( 'NONE',  ( 0.2923287055106771337, 0.2901785713310289783, 0.2123892367102621359 ) ) ;
#14890=CARTESIAN_POINT ( 'NONE',  ( -0.1116596296178200276, 0.2758928570453147433, 0.3436530038418508792 ) ) ;
#14906=VERTEX_POINT ( 'NONE', #3775 ) ;
#14911=CARTESIAN_POINT ( 'NONE',  ( 0.1236067977499789861, 0.1285714285714285310, -0.3804226065180614236 ) ) ;
#14919=CARTESIAN_POINT ( 'NONE',  ( -0.1236067977499789583, -0.01607142876651335150, -0.3804226065180614791 ) ) ;
#14920=CARTESIAN_POINT ( 'NONE',  ( 0.2434586614536247695, 1.857579423845308038E-17, -0.2752667295144964332 ) ) ;
#14940=CARTESIAN_POINT ( 'NONE',  ( -0.2923287055106771337, -0.04910714295468524004, -0.2123892367102620804 ) ) ;
#14943=CARTESIAN_POINT ( 'NONE',  ( 0.2923287055106771337, 0.09017857133102902267, -0.2123892367102620249 ) ) ;
#14948=VECTOR ( 'NONE', #2324, 39.37007874015748143 ) ;
#14959=CARTESIAN_POINT ( 'NONE',  ( 0.2233192592356400275, 0.07589285704531473220, -0.3073725909049499494 ) ) ;
#14961=ORIENTED_EDGE ( 'NONE', *, *, #20498, .T. ) ;
#14974=CARTESIAN_POINT ( 'NONE',  ( -0.3236067977499789694, 0.4196428569477722581, -0.2351141009169893104 ) ) ;
#14975=EDGE_CURVE ( 'NONE', #13117, #10268, #2368, .T. ) ;
#14982=CARTESIAN_POINT ( 'NONE',  ( -0.4000000000000000222, 0.2928571428571427604, -4.898587196589413075E-17 ) ) ;
#14998=ORIENTED_EDGE ( 'NONE', *, *, #14007, .T. ) ;
#14999=CARTESIAN_POINT ( 'NONE',  ( 2.326421213736078119E-17, 0.3866071427596002308, -0.3799334167787516425 ) ) ;
#15006=ORIENTED_EDGE ( 'NONE', *, *, #19439, .F. ) ;
#15012=CARTESIAN_POINT ( 'NONE',  ( -0.3613381517857144343, 0.2651785713310289005, 0.1174058825155740171 ) ) ;
#15017=CARTESIAN_POINT ( 'NONE',  ( 0.2472135954999579166, 0.3089285712334864931, 0.3402603233408160732 ) ) ;
#15030=DIRECTION ( 'NONE',  ( -0.000000000000000000, 0.000000000000000000, 1.000000000000000000 ) ) ;
#15031=CARTESIAN_POINT ( 'NONE',  ( 1.750236327630675475E-17, 0.3374999998049151295, -0.3999999999999999667 ) ) ;
#15033=CARTESIAN_POINT ( 'NONE',  ( 0.3236067977499790249, 0.2642857142857141795, -0.2351141009169892826 ) ) ;
#15042=CARTESIAN_POINT ( 'NONE',  ( -0.2472135954999579444, -0.01250000019508477368, -0.3402603233408159622 ) ) ;
#15064=CARTESIAN_POINT ( 'NONE',  ( -0.2233192592356399442, 0.1616071427596004473, -0.3073725909049500049 ) ) ;
#15066=VERTEX_POINT ( 'NONE', #832 ) ;
#15067=CARTESIAN_POINT ( 'NONE',  ( -6.979263641208234666E-17, 0.1366071427596004251, 0.3799334167787516980 ) ) ;
#15080=EDGE_LOOP ( 'NONE', ( #18732, #6001, #16046, #4766 ) ) ;
#15081=CARTESIAN_POINT ( 'NONE',  ( 0.3613381517857143232, 0.1330357141881718941, 0.1174058825155741975 ) ) ;
#15104=CARTESIAN_POINT ( 'NONE',  ( -0.3236067977499790249, 0.2999999999999999334, 0.2351141009169892271 ) ) ;
#15119=CARTESIAN_POINT ( 'NONE',  ( -0.1116596296178199582, 0.1758928570453147100, -0.3436530038418508792 ) ) ;
#15148=PLANE ( 'NONE',  #22060 ) ;
#15149=CARTESIAN_POINT ( 'NONE',  ( -0.2472135954999579999, 0.008928571233486629066, 0.3402603233408160732 ) ) ;
#15150=CARTESIAN_POINT ( 'NONE',  ( -0.3999999999999999667, 0.1464285714285713802, -0.1299678784931626030 ) ) ;
#15157=CARTESIAN_POINT ( 'NONE',  ( 0.3999999999999999667, 0.1732142855192008724, 0.1299678784931626307 ) ) ;
#15160=FACE_OUTER_BOUND ( 'NONE', #8929, .T. ) ;
#15178=CARTESIAN_POINT ( 'NONE',  ( -0.2233192592356399442, 0.01874999990245759460, -0.3073725909049500049 ) ) ;
#15180=CARTESIAN_POINT ( 'NONE',  ( 0.2923287055106771337, 0.1473214284738861568, 0.2123892367102621359 ) ) ;
#15193=CARTESIAN_POINT ( 'NONE',  ( -6.979263641208234666E-17, 0.1187499999024575897, 0.3799334167787516980 ) ) ;
#15199=CARTESIAN_POINT ( 'NONE',  ( 0.2977100099089716734, 3.659999999999999698, -0.09499999999999995948 ) ) ;
#15216=DIRECTION ( 'NONE',  ( 1.000000000000000000, 0.000000000000000000, 0.000000000000000000 ) ) ;
#15234=CARTESIAN_POINT ( 'NONE',  ( 2.326421213736078119E-17, 0.08303571418817184968, -0.3799334167787516425 ) ) ;
#15262=CARTESIAN_POINT ( 'NONE',  ( 0.06335377612981453466, 0.2731694899447553726, -0.3999999999999999667 ) ) ;
#15268=CARTESIAN_POINT ( 'NONE',  ( -0.2472135954999579444, 0.2107142857142856318, -0.3402603233408159622 ) ) ;
#15275=CARTESIAN_POINT ( 'NONE',  ( -0.3999999999999999667, 0.3517857140906293645, -0.1299678784931626030 ) ) ;
#15282=CARTESIAN_POINT ( 'NONE',  ( 9.101228903679513089E-16, 0.3017857140906293756, 0.4000000000000000222 ) ) ;
#15295=LINE ( 'NONE', #6012, #22959 ) ;
#15297=CARTESIAN_POINT ( 'NONE',  ( -0.4749999999999999778, 3.575000000000000622, 0.09499999999999995948 ) ) ;
#15298=CARTESIAN_POINT ( 'NONE',  ( 0.3613381517857143232, 0.06874999990245758696, -0.1174058825155740587 ) ) ;
#15301=CARTESIAN_POINT ( 'NONE',  ( -0.2923287055106771337, 0.4116071427596003640, 0.2123892367102619971 ) ) ;
#15314=CARTESIAN_POINT ( 'NONE',  ( -0.1116596296178200276, 0.1151785713310290032, 0.3436530038418508792 ) ) ;
#15317=ORIENTED_EDGE ( 'NONE', *, *, #2636, .T. ) ;
#15339=CARTESIAN_POINT ( 'NONE',  ( -0.06335377612981449302, 0.2768305100552443943, -0.4000000000000000222 ) ) ;
#15341=VERTEX_POINT ( 'NONE', #1265 ) ;
#15351=CARTESIAN_POINT ( 'NONE',  ( 0.3613381517857143232, -0.006250000097542392913, 0.000000000000000000 ) ) ;
#15357=VECTOR ( 'NONE', #19347, 39.37007874015748143 ) ;
#15359=CARTESIAN_POINT ( 'NONE',  ( 0.3999999999999999667, 0.1089285712334865930, -0.1299678784931625197 ) ) ;
#15360=CARTESIAN_POINT ( 'NONE',  ( -0.3039006371514270666, -1.707404996040164820E-17, -0.2596894543520890108 ) ) ;
#15366=LINE ( 'NONE', #22795, #14948 ) ;
#15368=EDGE_LOOP ( 'NONE', ( #8844, #17395, #19115, #18541 ) ) ;
#15372=CARTESIAN_POINT ( 'NONE',  ( -0.2233192592356400275, 0.3258928570453145102, 0.3073725909049499494 ) ) ;
#15384=CARTESIAN_POINT ( 'NONE',  ( 0.3613381517857143232, -0.05982142866897096484, 0.000000000000000000 ) ) ;
#15388=CARTESIAN_POINT ( 'NONE',  ( 0.1236067977499789028, 0.09999999999999997780, 0.3804226065180614791 ) ) ;
#15396=CARTESIAN_POINT ( 'NONE',  ( -0.1236067977499789583, 0.1982142855192009223, -0.3804226065180614791 ) ) ;
#15408=CIRCLE ( 'NONE', #18516, 0.3125000000000000000 ) ;
#15418=CARTESIAN_POINT ( 'NONE',  ( -0.1116596296178199582, 0.01517857133102903239, -0.3436530038418508792 ) ) ;
#15422=CARTESIAN_POINT ( 'NONE',  ( 0.2923287055106771337, 0.2901785713310289783, 0.2123892367102621359 ) ) ;
#15431=EDGE_CURVE ( 'NONE', #13196, #23444, #12931, .T. ) ;
#15435=CARTESIAN_POINT ( 'NONE',  ( 0.1116596296178199860, 0.2937499999024575925, -0.3436530038418508792 ) ) ;
#15438=ORIENTED_EDGE ( 'NONE', *, *, #5933, .F. ) ;
#15447=CARTESIAN_POINT ( 'NONE',  ( 0.000000000000000000, 3.700000000000000622, -0.4000000000000000222 ) ) ;
#15457=CARTESIAN_POINT ( 'NONE',  ( 0.3394572874457115752, 3.700000000000000622, -0.09499999999999993172 ) ) ;
#15461=CARTESIAN_POINT ( 'NONE',  ( -0.4000000000000000222, 0.2249999999999999223, 0.1299678784931624920 ) ) ;
#15465=EDGE_LOOP ( 'NONE', ( #755, #19296, #12995, #10413 ) ) ;
#15471=CARTESIAN_POINT ( 'NONE',  ( 0.3613381517857143232, -0.002678571526113826800, -0.1174058825155740587 ) ) ;
#15491=CARTESIAN_POINT ( 'NONE',  ( -0.2233192592356400275, 0.3973214284738861291, 0.3073725909049499494 ) ) ;
#15497=CARTESIAN_POINT ( 'NONE',  ( -0.4749999999999999778, 3.700000000000000622, 0.09499999999999995948 ) ) ;
#15505=CARTESIAN_POINT ( 'NONE',  ( -0.4000000000000000222, 0.1499999999999999667, -4.898587196589413075E-17 ) ) ;
#15506=CARTESIAN_POINT ( 'NONE',  ( 0.1236067977499789028, 0.3857142857142856207, 0.3804226065180614791 ) ) ;
#15515=CARTESIAN_POINT ( 'NONE',  ( 0.3236067977499789694, 0.2410714283763437660, 0.2351141009169893659 ) ) ;
#15520=DIRECTION ( 'NONE',  ( -1.000000000000000000, 0.000000000000000000, -0.000000000000000000 ) ) ;
#15527=CARTESIAN_POINT ( 'NONE',  ( 0.1236067977499789028, 0.3142857142857142239, 0.3804226065180614791 ) ) ;
#15531=CARTESIAN_POINT ( 'NONE',  ( -0.4000000000000000222, 0.007142857142857113144, -4.898587196589413075E-17 ) ) ;
#15534=CARTESIAN_POINT ( 'NONE',  ( 0.2233192592356399164, 0.1973214284738861179, 0.3073725909049500604 ) ) ;
#15537=CARTESIAN_POINT ( 'NONE',  ( -0.1116596296178200276, 0.3473214284738860846, 0.3436530038418508792 ) ) ;
#15541=( BOUNDED_CURVE ( )  B_SPLINE_CURVE ( 2, ( #23021, #13667, #15716, #20721, #19373, #21081, #4133, #15359, #7797, #22787, #8029, #5843, #356 ),
 .UNSPECIFIED., .F., .T. ) 
 B_SPLINE_CURVE_WITH_KNOTS ( ( 3, 2, 2, 2, 2, 2, 3 ),
 ( 0.2500000000000000000, 0.2571428571428571175, 0.2714285714285714080, 0.2857142857142856984, 0.2999999999999999889, 0.3142857142857142794, 0.3214285714285714524 ),
 .UNSPECIFIED. ) 
 CURVE ( )  GEOMETRIC_REPRESENTATION_ITEM ( )  RATIONAL_B_SPLINE_CURVE ( ( 0.9755282581475768211, 0.9755282581475768211, 1.000000000000000000, 0.9510565162951535312, 1.000000000000000000, 0.9510565162951535312, 1.000000000000000000, 0.9510565162951535312, 1.000000000000000000, 0.9510565162951535312, 1.000000000000000000, 0.9755282581475765991, 0.9755282581475767101 ) ) 
 REPRESENTATION_ITEM ( '' )  );
#15542=( BOUNDED_CURVE ( )  B_SPLINE_CURVE ( 2, ( #8172, #21468, #4752, #17332, #626, #8057, #15505, #13691, #4398, #17450, #21939, #18048, #23757 ),
 .UNSPECIFIED., .F., .F. ) 
 B_SPLINE_CURVE_WITH_KNOTS ( ( 3, 2, 2, 2, 2, 2, 3 ),
 ( 0.4642857142857143016, 0.4714285714285714191, 0.4857142857142857095, 0.5000000000000000000, 0.5142857142857142350, 0.5285714285714285809, 0.5357142857142856984 ),
 .UNSPECIFIED. ) 
 CURVE ( )  GEOMETRIC_REPRESENTATION_ITEM ( )  RATIONAL_B_SPLINE_CURVE ( ( 0.9755282581475767101, 0.9755282581475768211, 1.000000000000000000, 0.9510565162951535312, 1.000000000000000000, 0.9510565162951535312, 1.000000000000000000, 0.9510565162951535312, 1.000000000000000000, 0.9510565162951535312, 1.000000000000000000, 0.9755282581475768211, 0.9755282581475768211 ) ) 
 REPRESENTATION_ITEM ( '' )  );
#15578=AXIS2_PLACEMENT_3D ( 'NONE', #16220, #21462, #14146 ) ;
#15587=AXIS2_PLACEMENT_3D ( 'NONE', #17630, #23337, #21524 ) ;
#15588=CARTESIAN_POINT ( 'NONE',  ( 2.326421213736078119E-17, 0.01160714275960046671, -0.3799334167787516425 ) ) ;
#15597=DIRECTION ( 'NONE',  ( 1.000000000000000000, 0.000000000000000000, 0.000000000000000000 ) ) ;
#15602=B_SPLINE_CURVE_WITH_KNOTS ( 'NONE', 3,
 ( #4351, #23000, #6303, #18879 ),
 .UNSPECIFIED., .F., .F.,
 ( 4, 4 ),
 ( 1.008999589182314829E-06, 0.001469413801632195879 ),
 .UNSPECIFIED. ) ;
#15605=CARTESIAN_POINT ( 'NONE',  ( -0.2977100099089716734, 3.659999999999999698, -0.09499999999999995948 ) ) ;
#15613=VECTOR ( 'NONE', #10499, 39.37007874015748143 ) ;
#15627=CARTESIAN_POINT ( 'NONE',  ( -0.4000000000000000222, 0.3642857142857142128, -4.898587196589413075E-17 ) ) ;
#15635=CARTESIAN_POINT ( 'NONE',  ( -0.1236067977499790416, 0.2267857140906295033, 0.3804226065180614236 ) ) ;
#15646=CARTESIAN_POINT ( 'NONE',  ( 0.3236067977499789694, 0.4553571426620579565, 0.2351141009169893659 ) ) ;
#15652=DIRECTION ( 'NONE',  ( -8.881784197001252323E-16, 0.000000000000000000, 1.000000000000000000 ) ) ;
#15654=CARTESIAN_POINT ( 'NONE',  ( -0.2923287055106771337, 0.2366071427596004584, -0.2123892367102620804 ) ) ;
#15666=EDGE_CURVE ( 'NONE', #20523, #4205, #9473, .T. ) ;
#15678=PRODUCT_DEFINITION ( 'UNKNOWN', '', #8009, #2422 ) ;
#15685=FACE_OUTER_BOUND ( 'NONE', #23335, .T. ) ;
#15708=CARTESIAN_POINT ( 'NONE',  ( 0.2233192592356399997, 0.004464285616743319737, -0.3073725909049500049 ) ) ;
#15714=VERTEX_POINT ( 'NONE', #5642 ) ;
#15716=CARTESIAN_POINT ( 'NONE',  ( 0.1236067977499789028, 0.09107142837634375765, 0.3804226065180614791 ) ) ;
#15730=CARTESIAN_POINT ( 'NONE',  ( 0.1116596296178199027, 0.3366071427596004084, 0.3436530038418508792 ) ) ;
#15744=CARTESIAN_POINT ( 'NONE',  ( 0.2472135954999579166, 0.2464285714285713580, 0.3402603233408160732 ) ) ;
#15748=CARTESIAN_POINT ( 'NONE',  ( 0.3999999999999999667, 0.3249999999999997891, 0.1299678784931626307 ) ) ;
#15755=CARTESIAN_POINT ( 'NONE',  ( 0.3999999999999999667, 0.3874999998049151739, 0.1299678784931626307 ) ) ;
#15776=CARTESIAN_POINT ( 'NONE',  ( 0.2233192592356399997, 0.2901785713310290338, -0.3073725909049500049 ) ) ;
#15784=CARTESIAN_POINT ( 'NONE',  ( -0.2472135954999579444, 0.2017857140906293978, -0.3402603233408160732 ) ) ;
#15822=CARTESIAN_POINT ( 'NONE',  ( 0.2233192592356399997, 0.1473214284738861568, -0.3073725909049500049 ) ) ;
#15825=CYLINDRICAL_SURFACE ( 'NONE', #24023, 0.3125000000000000000 ) ;
#15840=CARTESIAN_POINT ( 'NONE',  ( 0.3059321453971730609, 2.458266394542412508E-17, 0.1926420918000893712 ) ) ;
#15856=CARTESIAN_POINT ( 'NONE',  ( -0.2923287055106771337, 0.1258928570453147211, 0.2123892367102619971 ) ) ;
#15861=CARTESIAN_POINT ( 'NONE',  ( 0.3999999999999999667, 0.3964285714285711859, 0.1299678784931626307 ) ) ;
#15865=LINE ( 'NONE', #12583, #13279 ) ;
#15868=CARTESIAN_POINT ( 'NONE',  ( 0.4000000000000000222, 0.4624999998049151850, 0.000000000000000000 ) ) ;
#15878=CARTESIAN_POINT ( 'NONE',  ( 0.000000000000000000, 0.000000000000000000, 0.000000000000000000 ) ) ;
#15879=VERTEX_POINT ( 'NONE', #5206 ) ;
#15887=AXIS2_PLACEMENT_3D ( 'NONE', #22194, #12958, #18420 ) ;
#15891=CARTESIAN_POINT ( 'NONE',  ( -0.3613381517857144343, 0.2473214284738860791, 0.1174058825155740171 ) ) ;
#15913=VECTOR ( 'NONE', #13358, 39.37007874015748143 ) ;
#15915=DIRECTION ( 'NONE',  ( 0.000000000000000000, 1.000000000000000000, 0.000000000000000000 ) ) ;
#15935=CARTESIAN_POINT ( 'NONE',  ( -0.2923287055106771337, 0.4116071427596003640, 0.2123892367102619971 ) ) ;
#15938=CARTESIAN_POINT ( 'NONE',  ( -0.2233192592356399442, 0.1616071427596004473, -0.3073725909049500049 ) ) ;
#15941=CARTESIAN_POINT ( 'NONE',  ( 0.000000000000000000, 3.700000000000000622, 0.000000000000000000 ) ) ;
#15951=AXIS2_PLACEMENT_3D ( 'NONE', #4294, #2479, #15520 ) ;
#15961=CARTESIAN_POINT ( 'NONE',  ( -0.2233192592356399442, 0.01874999990245759460, -0.3073725909049499494 ) ) ;
#15966=VECTOR ( 'NONE', #22400, 39.37007874015748143 ) ;
#15973=FACE_OUTER_BOUND ( 'NONE', #18119, .T. ) ;
#15975=CARTESIAN_POINT ( 'NONE',  ( 0.1116596296178199860, 0.1687499999024575648, -0.3436530038418508792 ) ) ;
#15979=CARTESIAN_POINT ( 'NONE',  ( -7.726019084026502927E-17, 0.3821428571428569509, 0.4205848896953069405 ) ) ;
#15982=VERTEX_POINT ( 'NONE', #19974 ) ;
#15988=CARTESIAN_POINT ( 'NONE',  ( 0.2923287055106771337, -0.05267857152611381266, -0.2123892367102620249 ) ) ;
#15994=CARTESIAN_POINT ( 'NONE',  ( 0.06335377612981468731, 0.1607590812887311205, 0.3999999999999999667 ) ) ;
#16000=ORIENTED_EDGE ( 'NONE', *, *, #1259, .F. ) ;
#16012=CARTESIAN_POINT ( 'NONE',  ( 4.898587196589413075E-17, 3.700000000000000622, 0.4000000000000000222 ) ) ;
#16014=CARTESIAN_POINT ( 'NONE',  ( -0.3613381517857144343, 0.3901785713310290116, 0.1174058825155740171 ) ) ;
#16023=CYLINDRICAL_SURFACE ( 'NONE', #9378, 0.4000000000000000222 ) ;
#16046=ORIENTED_EDGE ( 'NONE', *, *, #9294, .F. ) ;
#16060=ORIENTED_EDGE ( 'NONE', *, *, #10375, .T. ) ;
#16066=FACE_BOUND ( 'NONE', #1973, .T. ) ;
#16069=CARTESIAN_POINT ( 'NONE',  ( -0.2923287055106771337, 0.1651785713310290060, -0.2123892367102620804 ) ) ;
#16083=DIRECTION ( 'NONE',  ( -0.000000000000000000, -1.000000000000000000, -0.000000000000000000 ) ) ;
#16089=AXIS2_PLACEMENT_3D ( 'NONE', #12409, #8721, #16173 ) ;
#16098=CARTESIAN_POINT ( 'NONE',  ( 0.1116596296178199860, -0.04553571438325667436, -0.3436530038418508792 ) ) ;
#16107=CARTESIAN_POINT ( 'NONE',  ( -0.06335377612981472895, 0.06254479576953017594, -0.3999999999999999667 ) ) ;
#16111=CARTESIAN_POINT ( 'NONE',  ( -0.3613381517857143232, 0.04374999990245761333, -0.1174058825155741004 ) ) ;
#16115=EDGE_CURVE ( 'NONE', #15714, #16753, #19963, .T. ) ;
#16134=CARTESIAN_POINT ( 'NONE',  ( -0.3999999999999999667, 0.07499999999999995559, -0.1299678784931626030 ) ) ;
#16156=VECTOR ( 'NONE', #6215, 39.37007874015748143 ) ;
#16173=DIRECTION ( 'NONE',  ( 0.000000000000000000, 0.000000000000000000, 1.000000000000000000 ) ) ;
#16188=CARTESIAN_POINT ( 'NONE',  ( 0.3613381517857143232, 0.4366071427596004417, 0.1174058825155742114 ) ) ;
#16192=CARTESIAN_POINT ( 'NONE',  ( 0.3613381517857143232, 0.2758928570453146878, 0.1174058825155742114 ) ) ;
#16212=EDGE_CURVE ( 'NONE', #13263, #15341, #5293, .T. ) ;
#16220=CARTESIAN_POINT ( 'NONE',  ( -0.4749999999999999778, 3.575000000000000622, 2.908536147974962357E-17 ) ) ;
#16221=FACE_OUTER_BOUND ( 'NONE', #16663, .T. ) ;
#16222=CARTESIAN_POINT ( 'NONE',  ( -6.979263641208234666E-17, 0.1366071427596003973, 0.3799334167787516425 ) ) ;
#16231=VERTEX_POINT ( 'NONE', #15457 ) ;
#16236=CARTESIAN_POINT ( 'NONE',  ( 0.3613381517857143232, 0.008035714188171890621, 0.1174058825155742114 ) ) ;
#16240=ORIENTED_EDGE ( 'NONE', *, *, #13467, .T. ) ;
#16257=CARTESIAN_POINT ( 'NONE',  ( 0.3999999999999999667, -0.02500000000000002220, -0.1299678784931625475 ) ) ;
#16268=CARTESIAN_POINT ( 'NONE',  ( 0.000000000000000000, 3.700000000000000622, -0.4000000000000000222 ) ) ;
#16269=CARTESIAN_POINT ( 'NONE',  ( -0.06335377612981472895, 0.1964733670030168189, -0.3999999999999999667 ) ) ;
#16286=CARTESIAN_POINT ( 'NONE',  ( -0.4000000000000000222, 0.3678571428571427715, 0.1299678784931624920 ) ) ;
#16303=CARTESIAN_POINT ( 'NONE',  ( 0.3613381517857143232, 0.4401785713310289450, 0.000000000000000000 ) ) ;
#16305=VECTOR ( 'NONE', #20806, 39.37007874015748143 ) ;
#16307=CARTESIAN_POINT ( 'NONE',  ( 0.1236067977499789028, 0.02857142857142853584, 0.3804226065180614791 ) ) ;
#16308=CARTESIAN_POINT ( 'NONE',  ( -0.3613381517857143232, 0.2401785713310289894, -0.1174058825155741004 ) ) ;
#16313=EDGE_CURVE ( 'NONE', #21333, #5171, #8005, .T. ) ;
#16323=CARTESIAN_POINT ( 'NONE',  ( -0.06335377612981497875, 0.2054019386266730252, -0.3999999999999999667 ) ) ;
#16326=ORIENTED_EDGE ( 'NONE', *, *, #10608, .T. ) ;
#16340=CARTESIAN_POINT ( 'NONE',  ( -0.3613381517857143232, -0.02410714295468525253, -4.425116109941954795E-17 ) ) ;
#16351=CARTESIAN_POINT ( 'NONE',  ( -0.4000000000000000222, 0.08214285714285710083, 0.1299678784931624920 ) ) ;
#16355=CARTESIAN_POINT ( 'NONE',  ( -0.2923287055106771337, -0.01696428581182810383, 0.2123892367102619971 ) ) ;
#16379=CARTESIAN_POINT ( 'NONE',  ( -0.1236067977499789583, -0.007142857142857164318, -0.3804226065180614791 ) ) ;
#16383=AXIS2_PLACEMENT_3D ( 'NONE', #14365, #8379, #19973 ) ;
#16385=DIRECTION ( 'NONE',  ( 0.000000000000000000, 0.000000000000000000, 1.000000000000000000 ) ) ;
#16389=CARTESIAN_POINT ( 'NONE',  ( -0.1236067977499790416, 0.1553571426620580231, 0.3804226065180614236 ) ) ;
#16432=CARTESIAN_POINT ( 'NONE',  ( 0.2472135954999579721, 0.05357142857142854070, -0.3402603233408160732 ) ) ;
#16433=CARTESIAN_POINT ( 'NONE',  ( -0.2233192592356399442, 0.3758928570453146656, -0.3073725909049500049 ) ) ;
#16449=ORIENTED_EDGE ( 'NONE', *, *, #14975, .F. ) ;
#16454=EDGE_CURVE ( 'NONE', #9466, #431, #927, .T. ) ;
#16460=CARTESIAN_POINT ( 'NONE',  ( 0.1116596296178199027, 0.2116071427596004084, 0.3436530038418508792 ) ) ;
#16462=CARTESIAN_POINT ( 'NONE',  ( -0.4749999999999999778, 3.575000000000000622, 2.908536147974962357E-17 ) ) ;
#16475=CARTESIAN_POINT ( 'NONE',  ( 0.3613381517857143232, 0.2937499999024575370, 0.1174058825155742114 ) ) ;
#16477=CARTESIAN_POINT ( 'NONE',  ( 0.3084175934503982641, -2.427762526784286478E-18, -0.1882653658700420007 ) ) ;
#16483=CARTESIAN_POINT ( 'NONE',  ( 0.4000000000000000222, 0.3999999999999999112, 0.000000000000000000 ) ) ;
#16488=CARTESIAN_POINT ( 'NONE',  ( 0.1236067977499789861, 0.1999999999999999278, -0.3804226065180614236 ) ) ;
#16498=CARTESIAN_POINT ( 'NONE',  ( 0.3236067977499789694, 0.03571428571428568455, 0.2351141009169893659 ) ) ;
#16501=EDGE_CURVE ( 'NONE', #17619, #6124, #23464, .T. ) ;
#16505=CARTESIAN_POINT ( 'NONE',  ( 0.1236067977499789861, 0.1910714283763437493, -0.3804226065180614236 ) ) ;
#16506=CARTESIAN_POINT ( 'NONE',  ( -0.06335377612981435425, 0.1570980611782421266, 0.4000000000000000777 ) ) ;
#16521=LINE ( 'NONE', #1401, #5656 ) ;
#16525=CARTESIAN_POINT ( 'NONE',  ( 0.000000000000000000, 3.700000000000000622, 0.000000000000000000 ) ) ;
#16531=CARTESIAN_POINT ( 'NONE',  ( 0.2233192592356400275, 0.02232142847388617762, -0.3073725909049499494 ) ) ;
#16532=VERTEX_POINT ( 'NONE', #4819 ) ;
#16550=CARTESIAN_POINT ( 'NONE',  ( 0.4000000000000000222, 0.04285714285714282978, 0.000000000000000000 ) ) ;
#16552=CARTESIAN_POINT ( 'NONE',  ( -0.3613381517857144343, 0.3901785713310290116, 0.1174058825155740171 ) ) ;
#16580=CARTESIAN_POINT ( 'NONE',  ( -0.1116596296178199582, 0.3901785713310289561, -0.3436530038418508792 ) ) ;
#16593=CARTESIAN_POINT ( 'NONE',  ( 0.2233192592356399997, 0.1651785713310290615, -0.3073725909049500049 ) ) ;
#16617=CARTESIAN_POINT ( 'NONE',  ( 0.3613381517857143232, 0.4187499999024575370, 0.1174058825155742114 ) ) ;
#16624=CARTESIAN_POINT ( 'NONE',  ( 0.3999999999999999667, 0.03749999980491521001, -0.1299678784931625475 ) ) ;
#16626=ADVANCED_FACE ( 'NONE', ( #10212 ), #6535, .T. ) ;
#16643=ORIENTED_EDGE ( 'NONE', *, *, #6816, .F. ) ;
#16646=DIRECTION ( 'NONE',  ( -0.000000000000000000, -1.000000000000000000, -0.000000000000000000 ) ) ;
#16651=CARTESIAN_POINT ( 'NONE',  ( -0.2923287055106771337, 0.05446428561674331731, 0.2123892367102619971 ) ) ;
#16663=EDGE_LOOP ( 'NONE', ( #3607, #20346, #17044, #21648 ) ) ;
#16665=VERTEX_POINT ( 'NONE', #23587 ) ;
#16680=CARTESIAN_POINT ( 'NONE',  ( -0.4000000000000000222, 0.07321428551920090844, 0.1299678784931624920 ) ) ;
#16699=CARTESIAN_POINT ( 'NONE',  ( -6.979263641208234666E-17, 0.2794642856167432465, 0.3799334167787516425 ) ) ;
#16711=AXIS2_PLACEMENT_3D ( 'NONE', #23369, #23486, #6802 ) ;
#16712=CARTESIAN_POINT ( 'NONE',  ( -0.2233192592356399997, 0.2723214284738861291, 0.3073725909049499494 ) ) ;
#16717=EDGE_LOOP ( 'NONE', ( #7617, #21635, #764, #6151 ) ) ;
#16722=CARTESIAN_POINT ( 'NONE',  ( 0.3999999999999999667, 0.2517857140906293867, -0.1299678784931625197 ) ) ;
#16729=ORIENTED_EDGE ( 'NONE', *, *, #6958, .T. ) ;
#16733=CARTESIAN_POINT ( 'NONE',  ( -0.3236067977499789694, 0.2857142857142855874, -0.2351141009169893104 ) ) ;
#16740=ORIENTED_EDGE ( 'NONE', *, *, #6207, .T. ) ;
#16741=CARTESIAN_POINT ( 'NONE',  ( -0.2472135954999579444, 0.1303571426620580842, -0.3402603233408159622 ) ) ;
#16742=CARTESIAN_POINT ( 'NONE',  ( 0.1125251556717559304, 1.376365001936862257E-16, -0.3585253126667320434 ) ) ;
#16753=VERTEX_POINT ( 'NONE', #14838 ) ;
#16765=CARTESIAN_POINT ( 'NONE',  ( 0.2233192592356399997, 0.004464285616743319737, -0.3073725909049500049 ) ) ;
#16768=CARTESIAN_POINT ( 'NONE',  ( 0.1116596296178199860, 0.09732142847388618179, -0.3436530038418508792 ) ) ;
#16786=CARTESIAN_POINT ( 'NONE',  ( -0.3613381517857143788, 0.03303571418817188854, 0.1174058825155740310 ) ) ;
#16794=CARTESIAN_POINT ( 'NONE',  ( 0.3613381517857143232, 0.3473214284738860291, 0.1174058825155742114 ) ) ;
#16802=EDGE_CURVE ( 'NONE', #13969, #18530, #20906, .T. ) ;
#16822=( BOUNDED_CURVE ( )  B_SPLINE_CURVE ( 2, ( #7887, #15339, #4234, #11686, #9856, #18752, #14982, #216, #15104, #19111, #5819, #2414, #23230 ),
 .UNSPECIFIED., .F., .T. ) 
 B_SPLINE_CURVE_WITH_KNOTS ( ( 3, 2, 2, 2, 2, 2, 3 ),
 ( 0.7500000000000000000, 0.7571428571428571175, 0.7714285714285714635, 0.7857142857142856984, 0.8000000000000000444, 0.8142857142857142794, 0.8214285714285715079 ),
 .UNSPECIFIED. ) 
 CURVE ( )  GEOMETRIC_REPRESENTATION_ITEM ( )  RATIONAL_B_SPLINE_CURVE ( ( 0.9755282581475768211, 0.9755282581475768211, 1.000000000000000000, 0.9510565162951535312, 1.000000000000000000, 0.9510565162951535312, 1.000000000000000000, 0.9510565162951535312, 1.000000000000000000, 0.9510565162951535312, 1.000000000000000000, 0.9755282581475765991, 0.9755282581475768211 ) ) 
 REPRESENTATION_ITEM ( '' )  );
#16824=CARTESIAN_POINT ( 'NONE',  ( 0.3613381517857143232, 0.3687499999024574926, 0.000000000000000000 ) ) ;
#16827=CARTESIAN_POINT ( 'NONE',  ( 1.750236327630675475E-17, 0.05178571409062948661, -0.3999999999999999667 ) ) ;
#16834=CARTESIAN_POINT ( 'NONE',  ( -0.1116596296178199582, 0.1758928570453147100, -0.3436530038418508792 ) ) ;
#16837=CARTESIAN_POINT ( 'NONE',  ( 0.3532795013362199366, 1.447158556123030133E-17, -0.07948650416438482469 ) ) ;
#16842=EDGE_CURVE ( 'NONE', #9466, #21724, #502, .T. ) ;
#16849=VERTEX_POINT ( 'NONE', #4317 ) ;
#16852=CARTESIAN_POINT ( 'NONE',  ( -0.3236067977499790249, 0.005357142662058056448, 0.2351141009169892271 ) ) ;
#16853=CARTESIAN_POINT ( 'NONE',  ( 0.2472135954999579166, 0.3178571428571427826, 0.3402603233408160732 ) ) ;
#16862=CARTESIAN_POINT ( 'NONE',  ( -0.3999999999999999667, 0.06607142837634377708, -0.1299678784931626030 ) ) ;
#16880=CARTESIAN_POINT ( 'NONE',  ( -0.3613381517857144343, 0.03303571418817188854, 0.1174058825155740171 ) ) ;
#16883=CARTESIAN_POINT ( 'NONE',  ( -0.3613381517857143232, 0.1187499999024576036, -4.425116109941954795E-17 ) ) ;
#16897=CARTESIAN_POINT ( 'NONE',  ( -0.2923287055106771337, 0.03660714275960045422, 0.2123892367102619971 ) ) ;
#16906=CARTESIAN_POINT ( 'NONE',  ( -0.2233192592356399997, 0.3973214284738861291, 0.3073725909049499494 ) ) ;
#16925=LINE ( 'NONE', #2298, #7000 ) ;
#16935=CARTESIAN_POINT ( 'NONE',  ( -0.3613381517857143232, 0.1866071427596003585, -0.1174058825155741004 ) ) ;
#16948=CARTESIAN_POINT ( 'NONE',  ( 0.2472135954999579721, 0.4017857140906294644, -0.3402603233408160732 ) ) ;
#16966=CARTESIAN_POINT ( 'NONE',  ( 0.000000000000000000, 3.700000000000000622, 0.000000000000000000 ) ) ;
#16968=CARTESIAN_POINT ( 'NONE',  ( -0.3236067977499790249, 0.2285714285714285088, 0.2351141009169892271 ) ) ;
#16975=CARTESIAN_POINT ( 'NONE',  ( -0.3236067977499789694, 0.06249999980491521834, -0.2351141009169893104 ) ) ;
#16999=CARTESIAN_POINT ( 'NONE',  ( 2.326421213736078119E-17, -0.05982142866897093708, -0.3799334167787516425 ) ) ;
#17002=CARTESIAN_POINT ( 'NONE',  ( 0.2923287055106771337, 0.2187499999024575537, 0.2123892367102621359 ) ) ;
#17005=DIRECTION ( 'NONE',  ( 0.000000000000000000, 0.000000000000000000, 1.000000000000000000 ) ) ;
#17017=CARTESIAN_POINT ( 'NONE',  ( 0.1116596296178199027, 0.05089285704531473081, 0.3436530038418508792 ) ) ;
#17033=CARTESIAN_POINT ( 'NONE',  ( -9.626299801968715084E-16, 0.4089285712334866374, -0.4000000000000000222 ) ) ;
#17044=ORIENTED_EDGE ( 'NONE', *, *, #16802, .T. ) ;
#17046=VERTEX_POINT ( 'NONE', #6388 ) ;
#17055=ORIENTED_EDGE ( 'NONE', *, *, #14379, .F. ) ;
#17056=CARTESIAN_POINT ( 'NONE',  ( 0.3613381517857143232, 0.06874999990245758696, -0.1174058825155740587 ) ) ;
#17059=CARTESIAN_POINT ( 'NONE',  ( 0.1236067977499789861, 0.04821428551920090705, -0.3804226065180614236 ) ) ;
#17096=CARTESIAN_POINT ( 'NONE',  ( -0.1236067977499790416, 0.1642857142857142294, 0.3804226065180614236 ) ) ;
#17103=CARTESIAN_POINT ( 'NONE',  ( -0.1236067977499789583, 0.4124999998049151406, -0.3804226065180614791 ) ) ;
#17111=VECTOR ( 'NONE', #12168, 39.37007874015748143 ) ;
#17121=ORIENTED_EDGE ( 'NONE', *, *, #15666, .T. ) ;
#17127=CARTESIAN_POINT ( 'NONE',  ( 0.1116596296178199860, 0.008035714188171883682, -0.3436530038418508792 ) ) ;
#17130=CARTESIAN_POINT ( 'NONE',  ( 0.1116596296178199860, 0.3116071427596003862, -0.3436530038418508792 ) ) ;
#17136=CARTESIAN_POINT ( 'NONE',  ( 0.000000000000000000, 3.659999999999999698, 0.000000000000000000 ) ) ;
#17149=DIRECTION ( 'NONE',  ( 0.000000000000000000, 1.000000000000000000, 0.000000000000000000 ) ) ;
#17171=CARTESIAN_POINT ( 'NONE',  ( -0.06335377612981410445, 0.2374552042304697019, 0.4000000000000001887 ) ) ;
#17182=CARTESIAN_POINT ( 'NONE',  ( 0.2923287055106771337, 0.4330357141881717720, 0.2123892367102621359 ) ) ;
#17190=CARTESIAN_POINT ( 'NONE',  ( -0.05636693431585264313, -3.088309080874367638E-17, -0.3805424261366754934 ) ) ;
#17200=CARTESIAN_POINT ( 'NONE',  ( 0.2472135954999579721, 0.3303571426620581231, -0.3402603233408160732 ) ) ;
#17203=CARTESIAN_POINT ( 'NONE',  ( -6.979263641208234666E-17, 0.4044642856167431910, 0.3799334167787516980 ) ) ;
#17216=CARTESIAN_POINT ( 'NONE',  ( 0.2472135954999579721, 0.1249999999999999306, -0.3402603233408159622 ) ) ;
#17218=FACE_OUTER_BOUND ( 'NONE', #15080, .T. ) ;
#17227=CARTESIAN_POINT ( 'NONE',  ( 0.2472135954999579721, 0.3303571426620581231, -0.3402603233408159622 ) ) ;
#17233=ADVANCED_FACE ( 'NONE', ( #15160 ), #22593, .T. ) ;
#17240=ORIENTED_EDGE ( 'NONE', *, *, #22883, .F. ) ;
#17247=CARTESIAN_POINT ( 'NONE',  ( 0.2233192592356399997, 0.1473214284738861568, -0.3073725909049500049 ) ) ;
#17250=CARTESIAN_POINT ( 'NONE',  ( -0.3613381517857143232, 0.2580357141881718386, -0.1174058825155741143 ) ) ;
#17256=DIRECTION ( 'NONE',  ( -0.000000000000000000, -1.000000000000000000, -0.000000000000000000 ) ) ;
#17264=CARTESIAN_POINT ( 'NONE',  ( 0.1116596296178199860, 0.07946428561674331870, -0.3436530038418508792 ) ) ;
#17272=CARTESIAN_POINT ( 'NONE',  ( 0.000000000000000000, 3.700000000000000622, 0.000000000000000000 ) ) ;
#17282=CARTESIAN_POINT ( 'NONE',  ( -0.3716965727725675683, -7.597319298711556630E-17, 0.1377364605766528416 ) ) ;
#17296=CARTESIAN_POINT ( 'NONE',  ( -6.979263641208234666E-17, 0.4223214284738860402, 0.3799334167787516425 ) ) ;
#17306=CARTESIAN_POINT ( 'NONE',  ( -0.1174872052320808657, -2.846948999568485577E-18, -0.3695961464677890995 ) ) ;
#17317=CARTESIAN_POINT ( 'NONE',  ( -0.3613381517857143232, 0.3866071427596004528, -4.425116109941954795E-17 ) ) ;
#17329=CARTESIAN_POINT ( 'NONE',  ( 0.3394572874457115752, 3.700000000000000622, 0.09499999999999993172 ) ) ;
#17331=CARTESIAN_POINT ( 'NONE',  ( -0.4749999999999999778, 3.575000000000000622, 0.09499999999999995948 ) ) ;
#17332=CARTESIAN_POINT ( 'NONE',  ( -0.2472135954999579444, 0.1392857142857142350, -0.3402603233408160732 ) ) ;
#17335=EDGE_CURVE ( 'NONE', #23444, #18530, #10429, .T. ) ;
#17341=CARTESIAN_POINT ( 'NONE',  ( -0.2472135954999579999, 0.2946428569477723691, 0.3402603233408159622 ) ) ;
#17350=EDGE_CURVE ( 'NONE', #45, #17046, #2708, .T. ) ;
#17355=CARTESIAN_POINT ( 'NONE',  ( 0.1236067977499789028, 0.4482142855192008946, 0.3804226065180614791 ) ) ;
#17359=VERTEX_POINT ( 'NONE', #2593 ) ;
#17360=CARTESIAN_POINT ( 'NONE',  ( -0.4000000000000000222, 0.01071428571428569530, 0.1299678784931624920 ) ) ;
#17363=CARTESIAN_POINT ( 'NONE',  ( 0.2923287055106771337, 0.2866071427596004195, -0.2123892367102620249 ) ) ;
#17383=ORIENTED_EDGE ( 'NONE', *, *, #16842, .T. ) ;
#17395=ORIENTED_EDGE ( 'NONE', *, *, #21395, .F. ) ;
#17397=CARTESIAN_POINT ( 'NONE',  ( 0.3999999999999999667, -0.03392857162365620766, -0.1299678784931625475 ) ) ;
#17399=LINE ( 'NONE', #4589, #5618 ) ;
#17401=CARTESIAN_POINT ( 'NONE',  ( -0.3508668692247319254, -2.437189573335655702E-18, 0.1793730417398099186 ) ) ;
#17408=AXIS2_PLACEMENT_3D ( 'NONE', #16966, #19155, #5865 ) ;
#17416=CARTESIAN_POINT ( 'NONE',  ( 0.1116596296178199027, 0.05089285704531473081, 0.3436530038418508792 ) ) ;
#17436=CARTESIAN_POINT ( 'NONE',  ( -0.2923287055106771337, 0.3794642856167432798, -0.2123892367102620804 ) ) ;
#17447=CARTESIAN_POINT ( 'NONE',  ( 0.000000000000000000, 3.700000000000000622, -0.7199999999999994182 ) ) ;
#17450=CARTESIAN_POINT ( 'NONE',  ( -0.2472135954999579999, 0.1607142857142856429, 0.3402603233408160732 ) ) ;
#17454=DIRECTION ( 'NONE',  ( 0.000000000000000000, 0.000000000000000000, -1.000000000000000000 ) ) ;
#17459=CARTESIAN_POINT ( 'NONE',  ( 0.2472135954999579166, 0.2374999998049151795, 0.3402603233408160732 ) ) ;
#17469=( CONVERSION_BASED_UNIT ( 'INCH', #19415 ) LENGTH_UNIT ( ) NAMED_UNIT ( #22851 ) );
#17481=CARTESIAN_POINT ( 'NONE',  ( -0.2923287055106771337, 0.3794642856167432798, -0.2123892367102620804 ) ) ;
#17483=CARTESIAN_POINT ( 'NONE',  ( -0.2923287055106771337, 0.3973214284738861291, -0.2123892367102620804 ) ) ;
#17494=CARTESIAN_POINT ( 'NONE',  ( -0.2923287055106771337, 0.2508928570453147211, 0.2123892367102619971 ) ) ;
#17496=ORIENTED_EDGE ( 'NONE', *, *, #12302, .T. ) ;
#17517=CARTESIAN_POINT ( 'NONE',  ( -0.3250209672954003093, 7.507838726391275300E-19, 0.2186444650204283358 ) ) ;
#17524=AXIS2_PLACEMENT_3D ( 'NONE', #3604, #18484, #1778 ) ;
#17536=CARTESIAN_POINT ( 'NONE',  ( 0.2923287055106771337, -0.07053571438325667575, -0.2123892367102620249 ) ) ;
#17540=DIRECTION ( 'NONE',  ( 0.000000000000000000, 0.000000000000000000, 1.000000000000000000 ) ) ;
#17552=CARTESIAN_POINT ( 'NONE',  ( 0.1891708636127259202, 2.539511724522405989E-17, 0.3078630284654709781 ) ) ;
#17569=CARTESIAN_POINT ( 'NONE',  ( 0.06335377612981493711, 0.2411162243409586958, 0.3999999999999999667 ) ) ;
#17581=CARTESIAN_POINT ( 'NONE',  ( -7.726019084026502927E-17, 0.3017857140906293756, 0.4205848896953069405 ) ) ;
#17603=CARTESIAN_POINT ( 'NONE',  ( 0.2923287055106771337, 0.2008928570453147044, 0.2123892367102621359 ) ) ;
#17605=CARTESIAN_POINT ( 'NONE',  ( 0.3613381517857143232, 0.3723214284738861068, -0.1174058825155740587 ) ) ;
#17606=CARTESIAN_POINT ( 'NONE',  ( -0.3236067977499790249, 0.1482142855192009057, 0.2351141009169892271 ) ) ;
#17618=ORIENTED_EDGE ( 'NONE', *, *, #12902, .T. ) ;
#17619=VERTEX_POINT ( 'NONE', #11350 ) ;
#17624=EDGE_CURVE ( 'NONE', #21451, #16665, #4633, .T. ) ;
#17630=CARTESIAN_POINT ( 'NONE',  ( 0.000000000000000000, 2.735000000000000320, 0.000000000000000000 ) ) ;
#17654=CARTESIAN_POINT ( 'NONE',  ( 0.3613381517857143232, 0.1330357141881718941, 0.1174058825155742114 ) ) ;
#17663=CARTESIAN_POINT ( 'NONE',  ( 0.1236067977499789861, 0.1285714285714285310, -0.3804226065180614236 ) ) ;
#17672=CARTESIAN_POINT ( 'NONE',  ( 0.2094516944643866063, 2.389325547265710570E-17, 0.2954011803958429550 ) ) ;
#17677=CARTESIAN_POINT ( 'NONE',  ( 0.3008575146321451621, 0.0004514677251443983508, -0.2006503380323239050 ) ) ;
#17678=EDGE_CURVE ( 'NONE', #6978, #15714, #15366, .T. ) ;
#17696=CARTESIAN_POINT ( 'NONE',  ( 0.2977100099089716734, 3.659999999999999698, 0.09499999999999995948 ) ) ;
#17699=CARTESIAN_POINT ( 'NONE',  ( -0.3236067977499790249, 0.4339285712334866041, 0.2351141009169892271 ) ) ;
#17707=DIRECTION ( 'NONE',  ( 0.000000000000000000, 0.000000000000000000, 1.000000000000000000 ) ) ;
#17713=ORIENTED_EDGE ( 'NONE', *, *, #8118, .F. ) ;
#17722=CARTESIAN_POINT ( 'NONE',  ( -0.3613381517857144343, 0.3187499999024576147, 0.1174058825155740171 ) ) ;
#17749=AXIS2_PLACEMENT_3D ( 'NONE', #7572, #9771, #19146 ) ;
#17773=CARTESIAN_POINT ( 'NONE',  ( 0.000000000000000000, 0.000000000000000000, 0.000000000000000000 ) ) ;
#17774=CARTESIAN_POINT ( 'NONE',  ( 0.1116596296178199860, 0.1508928570453147155, -0.3436530038418508792 ) ) ;
#17791=CARTESIAN_POINT ( 'NONE',  ( 0.3457764953011678855, 1.003480569432279495E-17, 0.1075573247973250213 ) ) ;
#17808=CARTESIAN_POINT ( 'NONE',  ( 0.2923287055106771337, 0.1616071427596004473, -0.2123892367102620249 ) ) ;
#17817=EDGE_CURVE ( 'NONE', #4205, #13263, #8885, .T. ) ;
#17822=CARTESIAN_POINT ( 'NONE',  ( 0.1116596296178199860, 0.09732142847388618179, -0.3436530038418508792 ) ) ;
#17829=EDGE_CURVE ( 'NONE', #15066, #23116, #23259, .T. ) ;
#17847=CARTESIAN_POINT ( 'NONE',  ( 0.2233192592356399164, 0.2687499999024575703, 0.3073725909049500604 ) ) ;
#17851=CARTESIAN_POINT ( 'NONE',  ( -7.000945310522701902E-17, 0.1678571428571427882, 0.3999999999999999667 ) ) ;
#17854=CYLINDRICAL_SURFACE ( 'NONE', #10315, 0.7500000000000001110 ) ;
#17856=FACE_OUTER_BOUND ( 'NONE', #16717, .T. ) ;
#17860=ORIENTED_EDGE ( 'NONE', *, *, #21482, .T. ) ;
#17896=FACE_OUTER_BOUND ( 'NONE', #22889, .T. ) ;
#17897=CARTESIAN_POINT ( 'NONE',  ( -6.979263641208234666E-17, 0.2616071427596003973, 0.3799334167787516425 ) ) ;
#17925=DIRECTION ( 'NONE',  ( -0.000000000000000000, -1.000000000000000000, -0.000000000000000000 ) ) ;
#17927=CARTESIAN_POINT ( 'NONE',  ( -0.2923287055106771337, 0.05446428561674330343, 0.2123892367102619971 ) ) ;
#17937=CARTESIAN_POINT ( 'NONE',  ( -0.3236067977499789694, 0.07142857142857138297, -0.2351141009169893104 ) ) ;
#17938=DIRECTION ( 'NONE',  ( 0.000000000000000000, 0.000000000000000000, 1.000000000000000000 ) ) ;
#17941=CARTESIAN_POINT ( 'NONE',  ( -0.1116596296178199582, 0.03303571418817188854, -0.3436530038418508792 ) ) ;
#17946=CARTESIAN_POINT ( 'NONE',  ( 0.06335377612981431261, 0.1928123468925278527, -0.4000000000000000777 ) ) ;
#17958=ORIENTED_EDGE ( 'NONE', *, *, #10876, .T. ) ;
#17967=CARTESIAN_POINT ( 'NONE',  ( -0.3236067977499789694, 0.07142857142857138297, -0.2351141009169893104 ) ) ;
#17968=FACE_OUTER_BOUND ( 'NONE', #12838, .T. ) ;
#17973=CARTESIAN_POINT ( 'NONE',  ( -0.06335377612981472895, 0.1250447955744454220, -0.3999999999999999667 ) ) ;
#17979=CARTESIAN_POINT ( 'NONE',  ( -0.4000000000000000222, 0.2124999998049151573, -4.898587196589413075E-17 ) ) ;
#17982=ORIENTED_EDGE ( 'NONE', *, *, #7239, .T. ) ;
#18014=CARTESIAN_POINT ( 'NONE',  ( 0.1116596296178199860, 0.2937499999024575925, -0.3436530038418508792 ) ) ;
#18044=CARTESIAN_POINT ( 'NONE',  ( -0.1116596296178200276, 0.1330357141881718386, 0.3436530038418508792 ) ) ;
#18047=CYLINDRICAL_SURFACE ( 'NONE', #12750, 0.4000000000000000222 ) ;
#18048=CARTESIAN_POINT ( 'NONE',  ( -0.06335377612981457629, 0.1660266328018982773, 0.3999999999999999667 ) ) ;
#18053=CARTESIAN_POINT ( 'NONE',  ( -0.1236067977499790416, 0.09285714285714280480, 0.3804226065180614236 ) ) ;
#18057=CARTESIAN_POINT ( 'NONE',  ( 0.1116596296178199027, 0.06874999990245758696, 0.3436530038418508792 ) ) ;
#18070=EDGE_CURVE ( 'NONE', #13860, #7566, #21666, .T. ) ;
#18079=CARTESIAN_POINT ( 'NONE',  ( -0.4000000000000000222, 0.01071428571428569704, 0.1299678784931624920 ) ) ;
#18087=FACE_OUTER_BOUND ( 'NONE', #21386, .T. ) ;
#18091=LINE ( 'NONE', #6751, #5442 ) ;
#18107=VERTEX_POINT ( 'NONE', #17447 ) ;
#18119=EDGE_LOOP ( 'NONE', ( #17055, #19943, #7843, #22863 ) ) ;
#18134=CARTESIAN_POINT ( 'NONE',  ( -0.3613381517857144343, 0.3366071427596004084, 0.1174058825155740171 ) ) ;
#18138=CARTESIAN_POINT ( 'NONE',  ( -6.979263641208234666E-17, 0.1901785713310290005, 0.3799334167787516425 ) ) ;
#18145=CARTESIAN_POINT ( 'NONE',  ( 0.4000000000000000222, 0.1142857142857142405, 0.000000000000000000 ) ) ;
#18152=CARTESIAN_POINT ( 'NONE',  ( -9.626299801968715084E-16, 0.2035714285714284866, -0.4000000000000000222 ) ) ;
#18165=CARTESIAN_POINT ( 'NONE',  ( -0.2233192592356399997, 0.05803571418817187605, 0.3073725909049499494 ) ) ;
#18169=CARTESIAN_POINT ( 'NONE',  ( 0.2472135954999579166, 0.02321428551920091607, 0.3402603233408160732 ) ) ;
#18175=( BOUNDED_CURVE ( )  B_SPLINE_CURVE ( 2, ( #9481, #24102, #13162, #5455, #22399, #18503, #14613, #16680, #13039, #9361, #5699, #22521, #13278 ),
 .UNSPECIFIED., .F., .T. ) 
 B_SPLINE_CURVE_WITH_KNOTS ( ( 3, 2, 2, 2, 2, 2, 3 ),
 ( 0.1785714285714285754, 0.1857142857142857206, 0.2000000000000000111, 0.2142857142857142738, 0.2285714285714285643, 0.2428571428571428548, 0.2500000000000000000 ),
 .UNSPECIFIED. ) 
 CURVE ( )  GEOMETRIC_REPRESENTATION_ITEM ( )  RATIONAL_B_SPLINE_CURVE ( ( 0.9755282581475768211, 0.9755282581475768211, 1.000000000000000000, 0.9510565162951535312, 1.000000000000000000, 0.9510565162951535312, 1.000000000000000000, 0.9510565162951535312, 1.000000000000000000, 0.9510565162951535312, 1.000000000000000000, 0.9755282581475767101, 0.9755282581475768211 ) ) 
 REPRESENTATION_ITEM ( '' )  );
#18181=CARTESIAN_POINT ( 'NONE',  ( 0.3613381517857143232, 0.01160714275960046671, 0.000000000000000000 ) ) ;
#18202=CARTESIAN_POINT ( 'NONE',  ( -0.1116596296178200276, 0.4008928570453146878, 0.3436530038418508792 ) ) ;
#18211=EDGE_CURVE ( 'NONE', #4661, #13477, #9630, .T. ) ;
#18222=ORIENTED_EDGE ( 'NONE', *, *, #23996, .F. ) ;
#18234=CARTESIAN_POINT ( 'NONE',  ( -0.1236067977499790416, 0.3785714285714284477, 0.3804226065180614236 ) ) ;
#18243=CONICAL_SURFACE ( 'NONE', #22895, 0.7199999999999994182, 0.7853981633974506105 ) ;
#18245=ADVANCED_FACE ( 'NONE', ( #2342 ), #8983, .T. ) ;
#18256=CARTESIAN_POINT ( 'NONE',  ( 3.827021247335478926E-17, 0.02999999999999995379, 0.3125000000000000000 ) ) ;
#18274=VECTOR ( 'NONE', #9236, 39.37007874015748143 ) ;
#18285=CARTESIAN_POINT ( 'NONE',  ( -0.3613381517857144343, 0.2651785713310289005, 0.1174058825155740171 ) ) ;
#18289=CARTESIAN_POINT ( 'NONE',  ( 0.3999999999999999667, 0.03035714266205805437, 0.1299678784931626307 ) ) ;
#18299=CARTESIAN_POINT ( 'NONE',  ( 0.2923287055106771337, 0.1616071427596004473, -0.2123892367102620249 ) ) ;
#18302=DIRECTION ( 'NONE',  ( 0.000000000000000000, 0.000000000000000000, 1.000000000000000000 ) ) ;
#18320=CARTESIAN_POINT ( 'NONE',  ( -0.3999999999999999667, 0.003571428571428547031, -0.1299678784931626030 ) ) ;
#18328=CARTESIAN_POINT ( 'NONE',  ( -0.2472135954999579444, 0.05892857123348662490, -0.3402603233408159622 ) ) ;
#18346=VERTEX_POINT ( 'NONE', #18256 ) ;
#18355=CARTESIAN_POINT ( 'NONE',  ( 0.2233192592356400275, 0.2366071427596004029, -0.3073725909049499494 ) ) ;
#18405=CARTESIAN_POINT ( 'NONE',  ( -0.2233192592356399997, 0.3437499999024575814, 0.3073725909049499494 ) ) ;
#18417=CARTESIAN_POINT ( 'NONE',  ( -0.2233192592356399442, 0.1794642856167432965, -0.3073725909049500049 ) ) ;
#18420=DIRECTION ( 'NONE',  ( 0.000000000000000000, 0.000000000000000000, 1.000000000000000000 ) ) ;
#18427=CARTESIAN_POINT ( 'NONE',  ( 0.3999999999999999667, 0.1821428571428570509, 0.1299678784931626307 ) ) ;
#18432=CARTESIAN_POINT ( 'NONE',  ( -4.638126268221291196E-16, 0.06071428571428570675, -0.4000000000000000222 ) ) ;
#18437=LINE ( 'NONE', #7108, #14663 ) ;
#18439=CARTESIAN_POINT ( 'NONE',  ( 0.1236067977499789861, 0.05714285714285712720, -0.3804226065180614236 ) ) ;
#18440=CARTESIAN_POINT ( 'NONE',  ( 0.2977100099089716734, 3.700000000000000622, -0.09499999999999995948 ) ) ;
#18444=CARTESIAN_POINT ( 'NONE',  ( -0.3999999999999999667, 0.1374999998049151739, -0.1299678784931626030 ) ) ;
#18473=CARTESIAN_POINT ( 'NONE',  ( -0.2923287055106771337, 0.1258928570453147489, 0.2123892367102619971 ) ) ;
#18484=DIRECTION ( 'NONE',  ( -0.000000000000000000, -1.000000000000000000, -0.000000000000000000 ) ) ;
#18485=EDGE_LOOP ( 'NONE', ( #18222, #12536, #3337, #20912 ) ) ;
#18494=CARTESIAN_POINT ( 'NONE',  ( -0.3613381517857143232, 0.3866071427596004528, -4.425116109941954795E-17 ) ) ;
#18503=CARTESIAN_POINT ( 'NONE',  ( -0.3999999999999999667, 0.06607142837634374932, -0.1299678784931626030 ) ) ;
#18516=AXIS2_PLACEMENT_3D ( 'NONE', #2132, #18960, #17005 ) ;
#18524=CARTESIAN_POINT ( 'NONE',  ( -0.2233192592356399997, 0.2008928570453147322, 0.3073725909049499494 ) ) ;
#18530=VERTEX_POINT ( 'NONE', #11920 ) ;
#18536=CARTESIAN_POINT ( 'NONE',  ( 0.1116596296178199027, 0.1401785713310290393, 0.3436530038418508792 ) ) ;
#18541=ORIENTED_EDGE ( 'NONE', *, *, #16115, .F. ) ;
#18547=CARTESIAN_POINT ( 'NONE',  ( 0.3236067977499789694, 0.2410714283763437382, 0.2351141009169893659 ) ) ;
#18559=CARTESIAN_POINT ( 'NONE',  ( 0.3999999999999999667, 0.1107142857142856956, 0.1299678784931626307 ) ) ;
#18562=EDGE_CURVE ( 'NONE', #20999, #16665, #18982, .T. ) ;
#18568=CARTESIAN_POINT ( 'NONE',  ( 0.3236067977499789694, 0.02678571409062949910, 0.2351141009169893659 ) ) ;
#18579=CARTESIAN_POINT ( 'NONE',  ( -0.1236067977499790416, 0.2982142855192009279, 0.3804226065180614236 ) ) ;
#18596=CARTESIAN_POINT ( 'NONE',  ( 0.3613381517857143232, 0.08303571418817189131, 0.000000000000000000 ) ) ;
#18610=CARTESIAN_POINT ( 'NONE',  ( -0.1116596296178200276, 0.1866071427596004417, 0.3436530038418508792 ) ) ;
#18644=CARTESIAN_POINT ( 'NONE',  ( -0.2923287055106771337, 0.2687499999024575703, 0.2123892367102619971 ) ) ;
#18656=CARTESIAN_POINT ( 'NONE',  ( 0.2923287055106771337, 0.3044642856167432687, -0.2123892367102620249 ) ) ;
#18665=CARTESIAN_POINT ( 'NONE',  ( 0.000000000000000000, 3.700000000000000622, -0.4000000000000000222 ) ) ;
#18666=CARTESIAN_POINT ( 'NONE',  ( 0.06335377612981443751, 0.1696876529123872990, 0.4000000000000000222 ) ) ;
#18676=CARTESIAN_POINT ( 'NONE',  ( -0.4000000000000000222, 0.3589285712334865375, 0.1299678784931624920 ) ) ;
#18677=CARTESIAN_POINT ( 'NONE',  ( 0.1236067977499789861, 0.1999999999999999278, -0.3804226065180614236 ) ) ;
#18685=CARTESIAN_POINT ( 'NONE',  ( 0.1236067977499789861, 0.04821428551920092093, -0.3804226065180614236 ) ) ;
#18711=CARTESIAN_POINT ( 'NONE',  ( -0.3613381517857144343, 0.1044642856167432993, 0.1174058825155740171 ) ) ;
#18715=CARTESIAN_POINT ( 'NONE',  ( 2.326421213736078119E-17, 0.1008928570453146989, -0.3799334167787516980 ) ) ;
#18729=CARTESIAN_POINT ( 'NONE',  ( -0.1116596296178199582, 0.2294642856167432854, -0.3436530038418508792 ) ) ;
#18732=ORIENTED_EDGE ( 'NONE', *, *, #1891, .F. ) ;
#18738=EDGE_CURVE ( 'NONE', #20523, #15341, #2110, .T. ) ;
#18752=CARTESIAN_POINT ( 'NONE',  ( -0.3999999999999999667, 0.2892857142857141461, -0.1299678784931626030 ) ) ;
#18765=CARTESIAN_POINT ( 'NONE',  ( -0.2923287055106771337, 0.3973214284738861291, -0.2123892367102620804 ) ) ;
#18777=CARTESIAN_POINT ( 'NONE',  ( 0.000000000000000000, 0.02999999999999995379, 0.000000000000000000 ) ) ;
#18798=CARTESIAN_POINT ( 'NONE',  ( 0.3999999999999999667, 0.1821428571428570231, 0.1299678784931626307 ) ) ;
#18806=CARTESIAN_POINT ( 'NONE',  ( -0.1236067977499790416, 0.1553571426620580509, 0.3804226065180614236 ) ) ;
#18809=DIRECTION ( 'NONE',  ( -0.000000000000000000, -1.000000000000000000, -0.000000000000000000 ) ) ;
#18813=( BOUNDED_CURVE ( )  B_SPLINE_CURVE ( 2, ( #2718, #647, #15527, #4182, #22948, #19061, #10170, #6250, #13711, #12007, #6005, #21131, #2604 ),
 .UNSPECIFIED., .F., .T. ) 
 B_SPLINE_CURVE_WITH_KNOTS ( ( 3, 2, 2, 2, 2, 2, 3 ),
 ( 0.8214285714285715079, 0.8285714285714286254, 0.8428571428571428603, 0.8571428571428570953, 0.8714285714285714413, 0.8857142857142856762, 0.8928571428571429047 ),
 .UNSPECIFIED. ) 
 CURVE ( )  GEOMETRIC_REPRESENTATION_ITEM ( )  RATIONAL_B_SPLINE_CURVE ( ( 0.9755282581475768211, 0.9755282581475769321, 1.000000000000000000, 0.9510565162951535312, 1.000000000000000000, 0.9510565162951535312, 1.000000000000000000, 0.9510565162951535312, 1.000000000000000000, 0.9510565162951535312, 1.000000000000000000, 0.9755282581475765991, 0.9755282581475768211 ) ) 
 REPRESENTATION_ITEM ( '' )  );
#18831=CARTESIAN_POINT ( 'NONE',  ( 0.1116596296178199027, 0.1223214284738861762, 0.3436530038418508792 ) ) ;
#18834=CARTESIAN_POINT ( 'NONE',  ( -6.979263641208234666E-17, 0.2080357141881718774, 0.3799334167787516980 ) ) ;
#18838=AXIS2_PLACEMENT_3D ( 'NONE', #1260, #19793, #7233 ) ;
#18850=CARTESIAN_POINT ( 'NONE',  ( 2.326421213736078119E-17, 0.1544642856167433020, -0.3799334167787516980 ) ) ;
#18856=CARTESIAN_POINT ( 'NONE',  ( 0.000000000000000000, 3.700000000000000622, 0.000000000000000000 ) ) ;
#18866=CARTESIAN_POINT ( 'NONE',  ( -7.000945310522701902E-17, 0.4446428569477722803, 0.3999999999999999667 ) ) ;
#18871=CARTESIAN_POINT ( 'NONE',  ( -0.3917008400274854529, -3.329947049564607987E-18, 0.07871827179061374746 ) ) ;
#18879=CARTESIAN_POINT ( 'NONE',  ( -0.2977100099089716734, 3.659999999999999698, 0.09499999999999995948 ) ) ;
#18883=ADVANCED_FACE ( 'NONE', ( #17218 ), #5192, .T. ) ;
#18891=CARTESIAN_POINT ( 'NONE',  ( -0.3613381517857144343, 0.4080357141881717498, 0.1174058825155740171 ) ) ;
#18911=CARTESIAN_POINT ( 'NONE',  ( 2.326421213736078119E-17, 0.3687499999024574371, -0.3799334167787516980 ) ) ;
#18926=CARTESIAN_POINT ( 'NONE',  ( 9.101228903679513089E-16, 0.3732142855192008835, 0.4000000000000000222 ) ) ;
#18928=CARTESIAN_POINT ( 'NONE',  ( 0.3236067977499789694, 0.2499999999999999167, 0.2351141009169893659 ) ) ;
#18936=CARTESIAN_POINT ( 'NONE',  ( -0.3236067977499790249, 0.2910714283763437549, 0.2351141009169892271 ) ) ;
#18941=ORIENTED_EDGE ( 'NONE', *, *, #18562, .T. ) ;
#18944=CARTESIAN_POINT ( 'NONE',  ( -0.3236067977499789694, 0.2767857140906294644, -0.2351141009169893104 ) ) ;
#18956=CARTESIAN_POINT ( 'NONE',  ( 0.3613381517857143232, 0.06160714275960043479, 0.1174058825155742114 ) ) ;
#18959=CARTESIAN_POINT ( 'NONE',  ( 0.1116596296178199027, 0.4258928570453147100, 0.3436530038418508792 ) ) ;
#18960=DIRECTION ( 'NONE',  ( 0.000000000000000000, 1.000000000000000000, 0.000000000000000000 ) ) ;
#18982=LINE ( 'NONE', #15447, #20765 ) ;
#18994=CARTESIAN_POINT ( 'NONE',  ( -0.09343526663134765764, 1.673690498276180818E-18, 0.3656947149432163147 ) ) ;
#19012=CARTESIAN_POINT ( 'NONE',  ( -0.1116596296178199582, 0.01517857133102903239, -0.3436530038418508792 ) ) ;
#19027=CARTESIAN_POINT ( 'NONE',  ( 0.1236067977499789028, 0.3767857140906293867, 0.3804226065180614791 ) ) ;
#19043=CARTESIAN_POINT ( 'NONE',  ( -0.3236067977499790249, 0.3624999998049152072, 0.2351141009169892271 ) ) ;
#19044=CARTESIAN_POINT ( 'NONE',  ( -0.3999999999999999667, 0.2892857142857141461, -0.1299678784931626030 ) ) ;
#19052=CARTESIAN_POINT ( 'NONE',  ( -0.3236067977499790249, 0.3624999998049152072, 0.2351141009169892271 ) ) ;
#19057=CARTESIAN_POINT ( 'NONE',  ( -0.2472135954999579444, 0.2732142855192008501, -0.3402603233408160732 ) ) ;
#19061=CARTESIAN_POINT ( 'NONE',  ( 0.3999999999999999667, 0.3249999999999997891, 0.1299678784931626307 ) ) ;
#19067=CARTESIAN_POINT ( 'NONE',  ( 1.750236327630675475E-17, 0.2749999999999999112, -0.3999999999999999667 ) ) ;
#19069=CARTESIAN_POINT ( 'NONE',  ( -0.4749999999999999778, 3.575000000000000622, 2.908536147974962357E-17 ) ) ;
#19070=CARTESIAN_POINT ( 'NONE',  ( -0.2923287055106771337, 0.1080357141881718719, 0.2123892367102619971 ) ) ;
#19085=CARTESIAN_POINT ( 'NONE',  ( -0.3613381517857143232, 0.02946428561674330898, -4.425116109941954795E-17 ) ) ;
#19087=CIRCLE ( 'NONE', #5065, 0.7500000000000001110 ) ;
#19091=DIRECTION ( 'NONE',  ( 0.000000000000000000, -1.000000000000000000, 0.000000000000000000 ) ) ;
#19100=ORIENTED_EDGE ( 'NONE', *, *, #16313, .T. ) ;
#19102=CARTESIAN_POINT ( 'NONE',  ( -0.06335377612981457629, 0.4428123468925277417, 0.3999999999999999667 ) ) ;
#19111=CARTESIAN_POINT ( 'NONE',  ( -0.2472135954999579999, 0.3035714285714284366, 0.3402603233408160732 ) ) ;
#19115=ORIENTED_EDGE ( 'NONE', *, *, #1482, .T. ) ;
#19123=CARTESIAN_POINT ( 'NONE',  ( 0.2233192592356399164, -0.01696428581182810730, 0.3073725909049500604 ) ) ;
#19131=CARTESIAN_POINT ( 'NONE',  ( -0.009437680304838758777, 4.101846522467919178E-18, -0.3821420945942993752 ) ) ;
#19136=DIRECTION ( 'NONE',  ( 0.000000000000000000, 0.000000000000000000, -1.000000000000000000 ) ) ;
#19142=CARTESIAN_POINT ( 'NONE',  ( 0.3613381517857143232, 0.3473214284738860291, 0.1174058825155741975 ) ) ;
#19146=DIRECTION ( 'NONE',  ( 0.000000000000000000, 0.000000000000000000, 1.000000000000000000 ) ) ;
#19155=DIRECTION ( 'NONE',  ( 0.000000000000000000, 1.000000000000000000, 0.000000000000000000 ) ) ;
#19166=CARTESIAN_POINT ( 'NONE',  ( 0.3236067977499789694, 0.3124999998049152183, 0.2351141009169893659 ) ) ;
#19186=CARTESIAN_POINT ( 'NONE',  ( 0.3613381517857143232, -0.002678571526113826800, -0.1174058825155740587 ) ) ;
#19200=EDGE_CURVE ( 'NONE', #5943, #15066, #10696, .T. ) ;
#19207=CARTESIAN_POINT ( 'NONE',  ( 0.4749999999999999778, 3.700000000000000622, 0.09499999999999998723 ) ) ;
#19230=DIRECTION ( 'NONE',  ( 0.000000000000000000, -1.000000000000000000, 0.000000000000000000 ) ) ;
#19237=CARTESIAN_POINT ( 'NONE',  ( 1.750236327630675537E-16, 0.02499999999999997710, 0.3999999999999999667 ) ) ;
#19240=CARTESIAN_POINT ( 'NONE',  ( -0.2923287055106771337, 0.03660714275960045422, 0.2123892367102619971 ) ) ;
#19254=CYLINDRICAL_SURFACE ( 'NONE', #309, 0.4000000000000000222 ) ;
#19263=AXIS2_PLACEMENT_3D ( 'NONE', #14755, #1691, #11085 ) ;
#19272=ORIENTED_EDGE ( 'NONE', *, *, #12302, .F. ) ;
#19285=CARTESIAN_POINT ( 'NONE',  ( 0.3999999999999999667, 0.3946428569477722359, -0.1299678784931625475 ) ) ;
#19289=CARTESIAN_POINT ( 'NONE',  ( 0.3999999999999999667, 0.1732142855192008724, 0.1299678784931626307 ) ) ;
#19295=( NAMED_UNIT ( * ) PLANE_ANGLE_UNIT ( ) SI_UNIT ( $, .RADIAN. ) );
#19296=ORIENTED_EDGE ( 'NONE', *, *, #2030, .T. ) ;
#19310=CARTESIAN_POINT ( 'NONE',  ( 0.3613381517857143232, 0.3544642856167432576, -0.1174058825155740587 ) ) ;
#19315=CARTESIAN_POINT ( 'NONE',  ( -0.3613381517857143788, 0.4080357141881718053, 0.1174058825155740310 ) ) ;
#19330=EDGE_LOOP ( 'NONE', ( #4665, #7752, #6131, #9780, #8352, #10233, #20798, #11769, #21522, #3664, #23339, #23862, #10505, #13485, #10552, #11597, #8504 ) ) ;
#19332=ORIENTED_EDGE ( 'NONE', *, *, #23647, .F. ) ;
#19347=DIRECTION ( 'NONE',  ( -0.000000000000000000, -1.000000000000000000, -0.000000000000000000 ) ) ;
#19349=CARTESIAN_POINT ( 'NONE',  ( 0.04612308010668176445, 4.715469205126319992E-18, 0.3680979378183042439 ) ) ;
#19363=CARTESIAN_POINT ( 'NONE',  ( -0.3613381517857144343, -0.03839285724039952913, 0.1174058825155740171 ) ) ;
#19367=CARTESIAN_POINT ( 'NONE',  ( 0.3613381517857143232, 0.01517857133102903412, -0.1174058825155740587 ) ) ;
#19373=CARTESIAN_POINT ( 'NONE',  ( 0.3236067977499789694, 0.09821428551920090289, 0.2351141009169893659 ) ) ;
#19374=CARTESIAN_POINT ( 'NONE',  ( -0.02524939306089188373, -3.088309080874367638E-17, -0.3822476892351002742 ) ) ;
#19385=CARTESIAN_POINT ( 'NONE',  ( -0.2923287055106771337, 0.3223214284738861735, 0.2123892367102619971 ) ) ;
#19399=CARTESIAN_POINT ( 'NONE',  ( 0.2472135954999579166, 0.3892857142857142350, 0.3402603233408160732 ) ) ;
#19408=CARTESIAN_POINT ( 'NONE',  ( 2.575339694675500462E-17, 0.2660714283763437882, -0.4205848896953069405 ) ) ;
#19415=LENGTH_MEASURE_WITH_UNIT ( LENGTH_MEASURE( 0.02539999999999999897 ), #8071 );
#19425=CARTESIAN_POINT ( 'NONE',  ( 1.750236327630675537E-16, 0.02499999999999997710, 0.3999999999999999667 ) ) ;
#19427=CARTESIAN_POINT ( 'NONE',  ( 1.750236327630675475E-17, 0.3374999998049151295, -0.3999999999999999667 ) ) ;
#19428=CARTESIAN_POINT ( 'NONE',  ( 0.1116596296178199027, 0.1937499999024575870, 0.3436530038418508792 ) ) ;
#19429=LINE ( 'NONE', #23195, #15913 ) ;
#19430=CARTESIAN_POINT ( 'NONE',  ( -0.3613381517857143232, 0.4008928570453146878, -0.1174058825155741143 ) ) ;
#19432=CARTESIAN_POINT ( 'NONE',  ( -0.4000000000000000222, 0.1446428569477723469, 0.1299678784931624920 ) ) ;
#19439=EDGE_CURVE ( 'NONE', #7539, #17359, #8312, .T. ) ;
#19442=CARTESIAN_POINT ( 'NONE',  ( 0.2923287055106771337, 0.2866071427596004195, -0.2123892367102620249 ) ) ;
#19480=CARTESIAN_POINT ( 'NONE',  ( -0.3613381517857143232, 0.3116071427596003862, -0.1174058825155741004 ) ) ;
#19489=CARTESIAN_POINT ( 'NONE',  ( -0.07178572706788863278, 2.632010880910626829E-18, -0.3787435909716683757 ) ) ;
#19512=CARTESIAN_POINT ( 'NONE',  ( 0.3999999999999999667, 0.2607142857142855652, -0.1299678784931625197 ) ) ;
#19517=CARTESIAN_POINT ( 'NONE',  ( -0.3236067977499789694, 0.3571428571428570398, -0.2351141009169893104 ) ) ;
#19525=CARTESIAN_POINT ( 'NONE',  ( -6.979263641208234666E-17, -0.006250000097542391178, 0.3799334167787516425 ) ) ;
#19547=CARTESIAN_POINT ( 'NONE',  ( -0.2923287055106771337, 0.3080357141881718275, -0.2123892367102620804 ) ) ;
#19570=CARTESIAN_POINT ( 'NONE',  ( 0.4749999999999999778, 3.575000000000000622, 0.09499999999999998723 ) ) ;
#19573=CARTESIAN_POINT ( 'NONE',  ( 9.101228903679513089E-16, 0.3107142857142856096, 0.4000000000000000222 ) ) ;
#19575=ADVANCED_FACE ( 'NONE', ( #9875 ), #21080, .F. ) ;
#19595=CARTESIAN_POINT ( 'NONE',  ( -0.1116596296178200276, 0.2580357141881718941, 0.3436530038418508792 ) ) ;
#19600=CARTESIAN_POINT ( 'NONE',  ( 0.1891708636127259202, 2.539511724522405989E-17, 0.3078630284654709781 ) ) ;
#19629=CARTESIAN_POINT ( 'NONE',  ( 0.3613381517857143232, 0.1508928570453146878, 0.1174058825155742114 ) ) ;
#19633=DIRECTION ( 'NONE',  ( 0.000000000000000000, 0.000000000000000000, 1.000000000000000000 ) ) ;
#19634=DIRECTION ( 'NONE',  ( 0.000000000000000000, 0.000000000000000000, 1.000000000000000000 ) ) ;
#19638=CARTESIAN_POINT ( 'NONE',  ( 0.000000000000000000, 2.735000000000000320, 0.000000000000000000 ) ) ;
#19642=CARTESIAN_POINT ( 'NONE',  ( 0.3613381517857143232, 0.08660714275960043618, -0.1174058825155740587 ) ) ;
#19668=CARTESIAN_POINT ( 'NONE',  ( -0.1116596296178200276, 0.3294642856167432354, 0.3436530038418508792 ) ) ;
#19679=VERTEX_POINT ( 'NONE', #3259 ) ;
#19696=CLOSED_SHELL ( 'NONE', ( #4355, #18883, #5291, #3168, #13256, #9602, #16626, #7287, #11624, #4109, #6371, #12620, #6887, #17233, #6313, #4417, #9179, #2096, #22522, #14378, #7392, #2584, #13762, #21205, #126, #5162, #4358, #8135, #1916, #9472, #4245, #19575, #12670, #9868, #10227, #11357, #7427, #18245, #23162 ) ) ;
#19703=DIRECTION ( 'NONE',  ( -0.000000000000000000, -1.000000000000000000, -0.000000000000000000 ) ) ;
#19707=DIRECTION ( 'NONE',  ( 0.000000000000000000, 0.000000000000000000, 1.000000000000000000 ) ) ;
#19713=VECTOR ( 'NONE', #13155, 39.37007874015748143 ) ;
#19718=CARTESIAN_POINT ( 'NONE',  ( -0.2923287055106771337, 0.1794642856167432687, 0.2123892367102619971 ) ) ;
#19755=CARTESIAN_POINT ( 'NONE',  ( 2.326421213736078119E-17, -0.04196428581182810869, -0.3799334167787516425 ) ) ;
#19757=CARTESIAN_POINT ( 'NONE',  ( -0.4749999999999999778, 3.575000000000000622, 0.09499999999999995948 ) ) ;
#19758=DIRECTION ( 'NONE',  ( 0.000000000000000000, 0.7071067811865474617, 0.7071067811865474617 ) ) ;
#19767=CARTESIAN_POINT ( 'NONE',  ( -0.2233192592356399997, -0.01339285724039953294, 0.3073725909049499494 ) ) ;
#19772=CARTESIAN_POINT ( 'NONE',  ( 0.000000000000000000, 3.700000000000000622, -0.3125000000000000000 ) ) ;
#19773=ORIENTED_EDGE ( 'NONE', *, *, #4443, .T. ) ;
#19784=ORIENTED_EDGE ( 'NONE', *, *, #61, .T. ) ;
#19791=CARTESIAN_POINT ( 'NONE',  ( -6.979263641208234666E-17, 0.2616071427596003973, 0.3799334167787516425 ) ) ;
#19793=DIRECTION ( 'NONE',  ( 0.000000000000000000, 1.000000000000000000, 0.000000000000000000 ) ) ;
#19811=EDGE_CURVE ( 'NONE', #15879, #23116, #18175, .T. ) ;
#19838=CARTESIAN_POINT ( 'NONE',  ( 0.3613381517857143232, 0.2794642856167433020, 0.000000000000000000 ) ) ;
#19866=CIRCLE ( 'NONE', #5475, 0.3125000000000000000 ) ;
#19872=CARTESIAN_POINT ( 'NONE',  ( -0.3613381517857143232, 0.04732142847388615819, -4.425116109941954795E-17 ) ) ;
#19874=CARTESIAN_POINT ( 'NONE',  ( 0.000000000000000000, 3.700000000000000622, 0.000000000000000000 ) ) ;
#19880=CARTESIAN_POINT ( 'NONE',  ( -0.3999999999999999667, 0.07499999999999995559, -0.1299678784931626030 ) ) ;
#19886=CARTESIAN_POINT ( 'NONE',  ( 0.2923287055106771337, 0.01874999990245761194, -0.2123892367102620249 ) ) ;
#19898=CARTESIAN_POINT ( 'NONE',  ( -9.626299801968715084E-16, 0.2660714283763437327, -0.4000000000000000222 ) ) ;
#19912=CARTESIAN_POINT ( 'NONE',  ( -0.1236067977499790416, 0.02142857142857140795, 0.3804226065180614236 ) ) ;
#19928=EDGE_CURVE ( 'NONE', #2118, #12608, #568, .T. ) ;
#19943=ORIENTED_EDGE ( 'NONE', *, *, #17829, .T. ) ;
#19944=ORIENTED_EDGE ( 'NONE', *, *, #2636, .F. ) ;
#19956=EDGE_CURVE ( 'NONE', #21724, #18346, #17399, .T. ) ;
#19962=CARTESIAN_POINT ( 'NONE',  ( -0.3613381517857143232, 0.3330357141881718497, -4.425116109941954795E-17 ) ) ;
#19963=CIRCLE ( 'NONE', #13347, 0.7500000000000001110 ) ;
#19965=CARTESIAN_POINT ( 'NONE',  ( 0.2923287055106771337, 0.2008928570453147044, 0.2123892367102621359 ) ) ;
#19973=DIRECTION ( 'NONE',  ( 0.000000000000000000, 0.000000000000000000, 1.000000000000000000 ) ) ;
#19974=CARTESIAN_POINT ( 'NONE',  ( 0.3613381517857143232, 0.4223214284738860957, 0.000000000000000000 ) ) ;
#19978=CARTESIAN_POINT ( 'NONE',  ( 9.184850993605150903E-17, 2.735000000000000320, -0.7500000000000001110 ) ) ;
#19994=CARTESIAN_POINT ( 'NONE',  ( 0.1116596296178199027, 0.06874999990245758696, 0.3436530038418508792 ) ) ;
#20009=CARTESIAN_POINT ( 'NONE',  ( 2.326421213736078119E-17, 0.1008928570453146989, -0.3799334167787516425 ) ) ;
#20013=ORIENTED_EDGE ( 'NONE', *, *, #16842, .F. ) ;
#20022=CARTESIAN_POINT ( 'NONE',  ( 0.000000000000000000, 3.700000000000000622, -0.4000000000000000222 ) ) ;
#20023=CARTESIAN_POINT ( 'NONE',  ( 0.4749999999999999778, 3.575000000000000622, -0.09499999999999995948 ) ) ;
#20024=ORIENTED_EDGE ( 'NONE', *, *, #9760, .T. ) ;
#20026=ORIENTED_EDGE ( 'NONE', *, *, #12902, .F. ) ;
#20028=DIRECTION ( 'NONE',  ( 0.000000000000000000, -0.7071067811865459074, -0.7071067811865492381 ) ) ;
#20030=CARTESIAN_POINT ( 'NONE',  ( -0.3236067977499789694, -0.07142857142857143848, -0.2351141009169893104 ) ) ;
#20036=DIRECTION ( 'NONE',  ( 0.000000000000000000, 1.000000000000000000, 0.000000000000000000 ) ) ;
#20042=DIRECTION ( 'NONE',  ( -0.000000000000000000, -1.000000000000000000, -0.000000000000000000 ) ) ;
#20043=CARTESIAN_POINT ( 'NONE',  ( -0.1236067977499790416, 0.2267857140906294755, 0.3804226065180614236 ) ) ;
#20047=( BOUNDED_CURVE ( )  B_SPLINE_CURVE ( 2, ( #19600, #23015, #13769, #21195, #4486, #19367, #3842, #16531, #9209, #174, #9449, #9082, #5425, #20424, #3721, #24071, #16651, #1766, #14712, #22125, #2013, #14831, #7379, #11167, #18596, #51, #14943, #11043, #16768, #18715, #22247, #13131, #11284, #7616, #16883, #12892, #18473, #5545, #20662, #15067, #7735, #1887, #15180, #3959, #11402, #13247, #297, #13009, #22365, #9329, #3474, #7498, #5668, #20546, #22489, #5785, #23950, #9570, #7264, #18834, #20307, #2130, #17002, #4961, #10925, #12428, #20186, #18355, #1647, #3592, #13833, #6139, #20902, #17250, #13487, #9692, #10059, #6263, #8327, #23076, #5902, #534, #15422, #4431, #419, #13605, #11527, #4195, #17130, #13722, #8086, #896, #13361, #7971, #4556, #2729, #4072, #22617, #15537, #22961, #2381, #6018, #21143, #11898, #12018, #17605, #21020, #2258, #20781, #7852, #4313, #6384, #17483, #19430, #22849, #19315, #15301, #11768, #21266, #2616, #18959, #777, #10182, #22730, #11649 ),
 .UNSPECIFIED., .F., .F. ) 
 B_SPLINE_CURVE_WITH_KNOTS ( ( 3, 2, 2, 2, 2, 2, 2, 2, 2, 2, 2, 2, 2, 2, 2, 2, 2, 2, 2, 2, 2, 2, 2, 2, 2, 2, 2, 2, 2, 2, 2, 2, 2, 2, 2, 2, 2, 2, 2, 2, 2, 2, 2, 2, 2, 2, 2, 2, 2, 2, 2, 2, 2, 2, 2, 2, 2, 2, 2, 2, 2, 2, 3 ),
 ( 0.1196839499064063089, 0.1285714285714285587, 0.1428571428571428492, 0.1571428571428571397, 0.1714285714285714302, 0.1857142857142857206, 0.2000000000000000111, 0.2142857142857142738, 0.2285714285714285643, 0.2428571428571428825, 0.2571428571428571175, 0.2714285714285714080, 0.2857142857142856984, 0.2999999999999999889, 0.3142857142857142794, 0.3285714285714285698, 0.3428571428571428603, 0.3571428571428571508, 0.3714285714285714413, 0.3857142857142857317, 0.4000000000000000222, 0.4142857142857143127, 0.4285714285714285476, 0.4428571428571428381, 0.4571428571428571286, 0.4714285714285714191, 0.4857142857142857095, 0.4999999999999999445, 0.5142857142857142350, 0.5285714285714285809, 0.5428571428571428159, 0.5571428571428571619, 0.5714285714285713969, 0.5857142857142857428, 0.5999999999999999778, 0.6142857142857143238, 0.6285714285714285587, 0.6428571428571429047, 0.6571428571428571397, 0.6714285714285713746, 0.6857142857142857206, 0.6999999999999999556, 0.7142857142857143016, 0.7285714285714285365, 0.7428571428571428825, 0.7571428571428571175, 0.7714285714285714635, 0.7857142857142856984, 0.8000000000000000444, 0.8142857142857142794, 0.8285714285714286254, 0.8428571428571428603, 0.8571428571428570953, 0.8714285714285714413, 0.8857142857142857872, 0.9000000000000000222, 0.9142857142857142572, 0.9285714285714286031, 0.9428571428571428381, 0.9571428571428571841, 0.9714285714285715301, 0.9857142857142857650, 1.000000000000000000 ),
 .UNSPECIFIED. ) 
 CURVE ( )  GEOMETRIC_REPRESENTATION_ITEM ( )  RATIONAL_B_SPLINE_CURVE ( ( 0.9769881591460136683, 0.9695511082946919323, 1.000000000000000000, 0.9510565162951535312, 1.000000000000000000, 0.9510565162951535312, 1.000000000000000000, 0.9510565162951535312, 1.000000000000000000, 0.9510565162951535312, 1.000000000000000000, 0.9510565162951535312, 1.000000000000000000, 0.9510565162951535312, 1.000000000000000000, 0.9510565162951535312, 1.000000000000000000, 0.9510565162951535312, 1.000000000000000000, 0.9510565162951535312, 1.000000000000000000, 0.9510565162951535312, 1.000000000000000000, 0.9510565162951535312, 1.000000000000000000, 0.9510565162951535312, 1.000000000000000000, 0.9510565162951535312, 1.000000000000000000, 0.9510565162951535312, 1.000000000000000000, 0.9510565162951535312, 1.000000000000000000, 0.9510565162951535312, 1.000000000000000000, 0.9510565162951535312, 1.000000000000000000, 0.9510565162951535312, 1.000000000000000000, 0.9510565162951535312, 1.000000000000000000, 0.9510565162951535312, 1.000000000000000000, 0.9510565162951535312, 1.000000000000000000, 0.9510565162951535312, 1.000000000000000000, 0.9510565162951535312, 1.000000000000000000, 0.9510565162951535312, 1.000000000000000000, 0.9510565162951535312, 1.000000000000000000, 0.9510565162951535312, 1.000000000000000000, 0.9510565162951535312, 1.000000000000000000, 0.9510565162951535312, 1.000000000000000000, 0.9510565162951535312, 1.000000000000000000, 0.9510565162951535312, 1.000000000000000000, 0.9510565162951535312, 1.000000000000000000, 0.9510565162951535312, 1.000000000000000000, 0.9510565162951535312, 1.000000000000000000, 0.9510565162951535312, 1.000000000000000000, 0.9510565162951535312, 1.000000000000000000, 0.9510565162951535312, 1.000000000000000000, 0.9510565162951535312, 1.000000000000000000, 0.9510565162951535312, 1.000000000000000000, 0.9510565162951535312, 1.000000000000000000, 0.9510565162951535312, 1.000000000000000000, 0.9510565162951535312, 1.000000000000000000, 0.9510565162951535312, 1.000000000000000000, 0.9510565162951535312, 1.000000000000000000, 0.9510565162951535312, 1.000000000000000000, 0.9510565162951535312, 1.000000000000000000, 0.9510565162951535312, 1.000000000000000000, 0.9510565162951535312, 1.000000000000000000, 0.9510565162951535312, 1.000000000000000000, 0.9510565162951535312, 1.000000000000000000, 0.9510565162951535312, 1.000000000000000000, 0.9510565162951535312, 1.000000000000000000, 0.9510565162951535312, 1.000000000000000000, 0.9510565162951535312, 1.000000000000000000, 0.9510565162951535312, 1.000000000000000000, 0.9510565162951535312, 1.000000000000000000, 0.9510565162951535312, 1.000000000000000000, 0.9510565162951535312, 1.000000000000000000, 0.9510565162951535312, 1.000000000000000000, 0.9510565162951535312, 1.000000000000000000, 0.9510565162951535312, 1.000000000000000000, 0.9510565162951535312, 1.000000000000000000 ) ) 
 REPRESENTATION_ITEM ( '' )  );
#20057=ORIENTED_EDGE ( 'NONE', *, *, #13785, .T. ) ;
#20063=EDGE_CURVE ( 'NONE', #13477, #13733, #16822, .T. ) ;
#20087=CARTESIAN_POINT ( 'NONE',  ( -0.2923287055106771337, 0.3937499999024575148, 0.2123892367102619971 ) ) ;
#20112=CARTESIAN_POINT ( 'NONE',  ( 0.3613381517857143232, 0.4401785713310289450, 0.000000000000000000 ) ) ;
#20116=CARTESIAN_POINT ( 'NONE',  ( -0.2923287055106771337, -0.03125000009754239777, -0.2123892367102620804 ) ) ;
#20119=LINE ( 'NONE', #12704, #23617 ) ;
#20124=CARTESIAN_POINT ( 'NONE',  ( -0.2472135954999579999, 0.08928571428571424606, 0.3402603233408160732 ) ) ;
#20128=CARTESIAN_POINT ( 'NONE',  ( -0.2233192592356399997, 0.2008928570453147322, 0.3073725909049499494 ) ) ;
#20129=EDGE_LOOP ( 'NONE', ( #11857, #11882, #13782, #8601, #17860 ) ) ;
#20152=CARTESIAN_POINT ( 'NONE',  ( 0.2472135954999579721, -0.01785714285714287697, -0.3402603233408159622 ) ) ;
#20159=CARTESIAN_POINT ( 'NONE',  ( 0.4000000000000000222, -0.03750000019508477334, 0.000000000000000000 ) ) ;
#20165=LINE ( 'NONE', #16268, #9792 ) ;
#20186=CARTESIAN_POINT ( 'NONE',  ( 0.2923287055106771337, 0.2330357141881718719, -0.2123892367102620249 ) ) ;
#20200=FACE_OUTER_BOUND ( 'NONE', #6613, .T. ) ;
#20202=EDGE_CURVE ( 'NONE', #20558, #20678, #20428, .T. ) ;
#20210=CARTESIAN_POINT ( 'NONE',  ( 0.3613381517857143232, 0.3544642856167432576, -0.1174058825155740587 ) ) ;
#20219=DIRECTION ( 'NONE',  ( 0.000000000000000000, 0.000000000000000000, 1.000000000000000000 ) ) ;
#20235=CARTESIAN_POINT ( 'NONE',  ( 0.2977100099089716734, 3.700000000000000622, 0.09499999999999995948 ) ) ;
#20236=SHAPE_REPRESENTATION ( 'Aloris-BXA-Center-Shaft', ( #9127 ), #7955 ) ;
#20238=CARTESIAN_POINT ( 'NONE',  ( -6.979263641208234666E-17, 0.3508928570453145879, 0.3799334167787516425 ) ) ;
#20251=CARTESIAN_POINT ( 'NONE',  ( 0.2923287055106771337, 0.2330357141881718719, -0.2123892367102620249 ) ) ;
#20257=ORIENTED_EDGE ( 'NONE', *, *, #2467, .F. ) ;
#20273=CARTESIAN_POINT ( 'NONE',  ( 0.2472135954999579721, 0.05357142857142854764, -0.3402603233408159622 ) ) ;
#20281=CARTESIAN_POINT ( 'NONE',  ( 0.2472135954999579166, 0.1660714283763436994, 0.3402603233408160732 ) ) ;
#20307=CARTESIAN_POINT ( 'NONE',  ( 0.1116596296178199027, 0.2116071427596004639, 0.3436530038418508792 ) ) ;
#20319=CYLINDRICAL_SURFACE ( 'NONE', #17524, 0.4000000000000000222 ) ;
#20338=CARTESIAN_POINT ( 'NONE',  ( 4.898587196589413075E-17, 2.735000000000000320, 0.4000000000000000222 ) ) ;
#20341=CARTESIAN_POINT ( 'NONE',  ( 0.3394572874457115752, 3.700000000000000622, 0.09499999999999993172 ) ) ;
#20346=ORIENTED_EDGE ( 'NONE', *, *, #4838, .F. ) ;
#20356=CARTESIAN_POINT ( 'NONE',  ( 0.1116596296178199027, 0.2830357141881718053, 0.3436530038418508792 ) ) ;
#20368=CARTESIAN_POINT ( 'NONE',  ( 0.3613381517857143232, 0.2223214284738861402, 0.1174058825155742114 ) ) ;
#20370=VECTOR ( 'NONE', #12354, 39.37007874015748143 ) ;
#20377=CARTESIAN_POINT ( 'NONE',  ( 9.101228903679513089E-16, 0.3017857140906293756, 0.4000000000000000222 ) ) ;
#20390=DIRECTION ( 'NONE',  ( 0.000000000000000000, 1.000000000000000000, 0.000000000000000000 ) ) ;
#20392=CARTESIAN_POINT ( 'NONE',  ( -7.726019084026502927E-17, 0.2392857142857141295, 0.4205848896953069405 ) ) ;
#20393=LINE ( 'NONE', #18440, #359 ) ;
#20400=CARTESIAN_POINT ( 'NONE',  ( 0.3236067977499790249, 0.1124999998049151934, -0.2351141009169892826 ) ) ;
#20411=VERTEX_POINT ( 'NONE', #6122 ) ;
#20424=CARTESIAN_POINT ( 'NONE',  ( -0.3613381517857143232, 0.04374999990245761333, -0.1174058825155741143 ) ) ;
#20428=( BOUNDED_CURVE ( )  B_SPLINE_CURVE ( 2, ( #2111, #11509, #22598, #19057, #18944, #7950, #9801, #5770, #13231, #20643, #18579, #1869, #15282 ),
 .UNSPECIFIED., .F., .T. ) 
 B_SPLINE_CURVE_WITH_KNOTS ( ( 3, 2, 2, 2, 2, 2, 3 ),
 ( 0.6071428571428572063, 0.6142857142857143238, 0.6285714285714285587, 0.6428571428571429047, 0.6571428571428571397, 0.6714285714285713746, 0.6785714285714286031 ),
 .UNSPECIFIED. ) 
 CURVE ( )  GEOMETRIC_REPRESENTATION_ITEM ( )  RATIONAL_B_SPLINE_CURVE ( ( 0.9755282581475768211, 0.9755282581475769321, 1.000000000000000000, 0.9510565162951535312, 1.000000000000000000, 0.9510565162951535312, 1.000000000000000000, 0.9510565162951535312, 1.000000000000000000, 0.9510565162951535312, 1.000000000000000000, 0.9755282581475765991, 0.9755282581475768211 ) ) 
 REPRESENTATION_ITEM ( '' )  );
#20438=CARTESIAN_POINT ( 'NONE',  ( 0.2923287055106771337, 0.1294642856167433076, 0.2123892367102621359 ) ) ;
#20477=CARTESIAN_POINT ( 'NONE',  ( -0.3613381517857144343, 0.3366071427596004084, 0.1174058825155740171 ) ) ;
#20487=CARTESIAN_POINT ( 'NONE',  ( 0.1116596296178199860, 0.1687499999024575925, -0.3436530038418508792 ) ) ;
#20491=CARTESIAN_POINT ( 'NONE',  ( 0.3084175934503982641, -2.427762526784286478E-18, -0.1882653658700420007 ) ) ;
#20498=EDGE_CURVE ( 'NONE', #4780, #22531, #1720, .T. ) ;
#20511=CARTESIAN_POINT ( 'NONE',  ( -0.1236067977499789583, 0.3410714283763437438, -0.3804226065180614791 ) ) ;
#20512=CARTESIAN_POINT ( 'NONE',  ( 0.1236067977499789028, 0.2428571428571427715, 0.3804226065180614791 ) ) ;
#20519=CARTESIAN_POINT ( 'NONE',  ( -0.2472135954999579999, 0.08035714266205805367, 0.3402603233408159622 ) ) ;
#20523=VERTEX_POINT ( 'NONE', #8430 ) ;
#20527=( BOUNDED_CURVE ( )  B_SPLINE_CURVE ( 2, ( #14126, #1075, #6559, #8632, #23489, #12552, #18145, #21555, #2782, #21324, #17663, #4846, #5084 ),
 .UNSPECIFIED., .F., .T. ) 
 B_SPLINE_CURVE_WITH_KNOTS ( ( 3, 2, 2, 2, 2, 2, 3 ),
 ( 0.3928571428571429047, 0.4000000000000000222, 0.4142857142857143127, 0.4285714285714285476, 0.4428571428571428381, 0.4571428571428571286, 0.4642857142857143016 ),
 .UNSPECIFIED. ) 
 CURVE ( )  GEOMETRIC_REPRESENTATION_ITEM ( )  RATIONAL_B_SPLINE_CURVE ( ( 0.9755282581475767101, 0.9755282581475768211, 1.000000000000000000, 0.9510565162951535312, 1.000000000000000000, 0.9510565162951535312, 1.000000000000000000, 0.9510565162951535312, 1.000000000000000000, 0.9510565162951535312, 1.000000000000000000, 0.9755282581475765991, 0.9755282581475767101 ) ) 
 REPRESENTATION_ITEM ( '' )  );
#20544=CARTESIAN_POINT ( 'NONE',  ( 0.2923287055106771337, 0.05803571418817188299, 0.2123892367102621359 ) ) ;
#20546=CARTESIAN_POINT ( 'NONE',  ( -0.3613381517857143232, 0.1866071427596004140, -0.1174058825155741143 ) ) ;
#20558=VERTEX_POINT ( 'NONE', #2951 ) ;
#20559=CARTESIAN_POINT ( 'NONE',  ( -0.3613381517857143232, 0.09732142847388614015, -0.1174058825155741143 ) ) ;
#20561=ORIENTED_EDGE ( 'NONE', *, *, #2467, .T. ) ;
#20583=CARTESIAN_POINT ( 'NONE',  ( 9.101228903679513089E-16, 0.2392857142857141850, 0.4000000000000000222 ) ) ;
#20587=B_SPLINE_CURVE_WITH_KNOTS ( 'NONE', 3,
 ( #12991, #11145, #1630, #1747 ),
 .UNSPECIFIED., .F., .F.,
 ( 4, 4 ),
 ( 0.02048720093474762707, 0.02195606945063139845 ),
 .UNSPECIFIED. ) ;
#20595=CARTESIAN_POINT ( 'NONE',  ( -0.2923287055106771337, 0.3401785713310290227, 0.2123892367102619971 ) ) ;
#20598=CARTESIAN_POINT ( 'NONE',  ( 0.000000000000000000, 3.700000000000000622, 0.3525000000000007017 ) ) ;
#20627=CARTESIAN_POINT ( 'NONE',  ( 0.3999999999999999667, 0.1892857142857141961, -0.1299678784931625475 ) ) ;
#20634=CARTESIAN_POINT ( 'NONE',  ( -0.1236067977499790416, 0.08392857123348664017, 0.3804226065180614236 ) ) ;
#20643=CARTESIAN_POINT ( 'NONE',  ( -0.2472135954999579999, 0.2946428569477723136, 0.3402603233408160732 ) ) ;
#20654=EDGE_CURVE ( 'NONE', #18346, #17046, #21958, .T. ) ;
#20659=CARTESIAN_POINT ( 'NONE',  ( -0.2923287055106771337, 0.09374999990245758141, -0.2123892367102620804 ) ) ;
#20662=CARTESIAN_POINT ( 'NONE',  ( -0.1116596296178200276, 0.1330357141881718663, 0.3436530038418508792 ) ) ;
#20678=VERTEX_POINT ( 'NONE', #20377 ) ;
#20679=CARTESIAN_POINT ( 'NONE',  ( -0.3613381517857143232, 0.1008928570453147405, -4.425116109941954795E-17 ) ) ;
#20704=CARTESIAN_POINT ( 'NONE',  ( -0.3236067977499790249, 0.2285714285714285088, 0.2351141009169892271 ) ) ;
#20706=ORIENTED_EDGE ( 'NONE', *, *, #2030, .F. ) ;
#20713=VERTEX_POINT ( 'NONE', #851 ) ;
#20714=CARTESIAN_POINT ( 'NONE',  ( -0.3613381517857143232, 0.2580357141881718386, -0.1174058825155741004 ) ) ;
#20721=CARTESIAN_POINT ( 'NONE',  ( 0.2472135954999579166, 0.09464285694777231639, 0.3402603233408160732 ) ) ;
#20725=DIRECTION ( 'NONE',  ( -0.000000000000000000, -1.000000000000000000, -0.000000000000000000 ) ) ;
#20735=EDGE_CURVE ( 'NONE', #6859, #13196, #22921, .T. ) ;
#20744=ORIENTED_EDGE ( 'NONE', *, *, #7522, .T. ) ;
#20747=CARTESIAN_POINT ( 'NONE',  ( -0.1236067977499790416, 0.3696428569477722137, 0.3804226065180614236 ) ) ;
#20748=CARTESIAN_POINT ( 'NONE',  ( -0.3236067977499789694, 0.2142857142857142461, -0.2351141009169893104 ) ) ;
#20757=CARTESIAN_POINT ( 'NONE',  ( -0.2472135954999579999, 0.008928571233486644679, 0.3402603233408159622 ) ) ;
#20765=VECTOR ( 'NONE', #21166, 39.37007874015748143 ) ;
#20778=CARTESIAN_POINT ( 'NONE',  ( 0.3613381517857143232, 0.1330357141881718941, 0.1174058825155742114 ) ) ;
#20781=CARTESIAN_POINT ( 'NONE',  ( 0.1116596296178199860, 0.3830357141881718386, -0.3436530038418508792 ) ) ;
#20796=CARTESIAN_POINT ( 'NONE',  ( 0.1116596296178199860, 0.1508928570453147155, -0.3436530038418508792 ) ) ;
#20798=ORIENTED_EDGE ( 'NONE', *, *, #8568, .F. ) ;
#20806=DIRECTION ( 'NONE',  ( -1.000000000000000000, -0.000000000000000000, -0.000000000000000000 ) ) ;
#20818=CARTESIAN_POINT ( 'NONE',  ( -0.3583630266090071514, -7.597319298711557862E-17, 0.1657390341004710554 ) ) ;
#20833=VERTEX_POINT ( 'NONE', #12444 ) ;
#20834=CARTESIAN_POINT ( 'NONE',  ( 0.3613381517857143232, 0.06517857133102902822, 0.000000000000000000 ) ) ;
#20852=CARTESIAN_POINT ( 'NONE',  ( 0.4000000000000000222, 0.3196428569477723358, 0.000000000000000000 ) ) ;
#20868=CARTESIAN_POINT ( 'NONE',  ( 0.3999999999999999667, 0.2607142857142855652, -0.1299678784931625475 ) ) ;
#20876=CARTESIAN_POINT ( 'NONE',  ( -0.3999999999999999667, 0.2089285712334865985, -0.1299678784931626030 ) ) ;
#20895=DIRECTION ( 'NONE',  ( -1.000000000000000000, -0.000000000000000000, -0.000000000000000000 ) ) ;
#20898=CARTESIAN_POINT ( 'NONE',  ( 0.2233192592356399164, -0.01696428581182810730, 0.3073725909049500604 ) ) ;
#20902=CARTESIAN_POINT ( 'NONE',  ( -0.2923287055106771337, 0.2544642856167432798, -0.2123892367102620804 ) ) ;
#20906=LINE ( 'NONE', #22622, #4001 ) ;
#20910=EDGE_CURVE ( 'NONE', #20999, #3235, #5251, .T. ) ;
#20912=ORIENTED_EDGE ( 'NONE', *, *, #16802, .F. ) ;
#20915=CARTESIAN_POINT ( 'NONE',  ( 0.2923287055106771337, 0.1437499999024575981, -0.2123892367102620249 ) ) ;
#20931=ORIENTED_EDGE ( 'NONE', *, *, #19928, .T. ) ;
#20938=CARTESIAN_POINT ( 'NONE',  ( -0.1963981168484050244, -1.109535145422192752E-16, 0.3299405160370264545 ) ) ;
#20954=CARTESIAN_POINT ( 'NONE',  ( -0.2923287055106771337, 0.4116071427596003640, 0.2123892367102619971 ) ) ;
#20968=CARTESIAN_POINT ( 'NONE',  ( 0.2472135954999579166, 0.3803571426620580564, 0.3402603233408160732 ) ) ;
#20972=CARTESIAN_POINT ( 'NONE',  ( -0.3613381517857143232, 0.3151785713310290005, -4.425116109941954795E-17 ) ) ;
#20973=CARTESIAN_POINT ( 'NONE',  ( 0.000000000000000000, 3.700000000000000622, -0.4000000000000000222 ) ) ;
#20981=VECTOR ( 'NONE', #22164, 39.37007874015748143 ) ;
#20983=FACE_OUTER_BOUND ( 'NONE', #1133, .T. ) ;
#20985=CARTESIAN_POINT ( 'NONE',  ( 0.1236067977499789861, 0.3428571428571428048, -0.3804226065180614236 ) ) ;
#20993=CARTESIAN_POINT ( 'NONE',  ( -7.726019084026502927E-17, 0.2303571426620580065, 0.4205848896953069405 ) ) ;
#20999=VERTEX_POINT ( 'NONE', #23597 ) ;
#21007=CARTESIAN_POINT ( 'NONE',  ( 0.2472135954999579166, 0.4517857140906293423, 0.3402603233408160732 ) ) ;
#21015=CARTESIAN_POINT ( 'NONE',  ( -6.979263641208234666E-17, -0.02410714295468524906, 0.3799334167787516425 ) ) ;
#21020=CARTESIAN_POINT ( 'NONE',  ( 0.2923287055106771337, 0.3758928570453146656, -0.2123892367102620249 ) ) ;
#21029=ORIENTED_EDGE ( 'NONE', *, *, #9294, .T. ) ;
#21032=CARTESIAN_POINT ( 'NONE',  ( -0.2233192592356399442, 0.3044642856167432132, -0.3073725909049499494 ) ) ;
#21040=CARTESIAN_POINT ( 'NONE',  ( 0.3116633505738114485, 3.673292957400295933, -0.09499999999999995948 ) ) ;
#21073=CARTESIAN_POINT ( 'NONE',  ( 0.2233192592356399164, 0.4294642856167432687, 0.3073725909049500604 ) ) ;
#21080=PLANE ( 'NONE',  #9507 ) ;
#21081=CARTESIAN_POINT ( 'NONE',  ( 0.3999999999999999667, 0.1017857140906294616, 0.1299678784931626307 ) ) ;
#21082=CARTESIAN_POINT ( 'NONE',  ( 0.3084175934503982641, -2.427762526784286478E-18, -0.1882653658700420007 ) ) ;
#21110=CARTESIAN_POINT ( 'NONE',  ( -0.4000000000000000222, 0.3678571428571427715, 0.1299678784931624920 ) ) ;
#21118=CARTESIAN_POINT ( 'NONE',  ( 0.3999999999999999667, 0.3160714283763437216, 0.1299678784931626307 ) ) ;
#21131=CARTESIAN_POINT ( 'NONE',  ( 0.06335377612981404893, 0.3445980613733267695, -0.4000000000000001887 ) ) ;
#21139=CARTESIAN_POINT ( 'NONE',  ( -0.3613381517857143232, 0.3116071427596003862, -0.1174058825155741004 ) ) ;
#21143=CARTESIAN_POINT ( 'NONE',  ( 0.2923287055106771337, 0.3616071427596004306, 0.2123892367102621359 ) ) ;
#21150=AXIS2_PLACEMENT_3D ( 'NONE', #17136, #11532, #13725 ) ;
#21166=DIRECTION ( 'NONE',  ( -0.000000000000000000, -1.000000000000000000, -0.000000000000000000 ) ) ;
#21177=CARTESIAN_POINT ( 'NONE',  ( -0.0003315323776482123944, 4.715469205126314599E-18, 0.3725069824736144675 ) ) ;
#21192=CARTESIAN_POINT ( 'NONE',  ( -0.2233192592356399442, 0.09017857133102905043, -0.3073725909049500049 ) ) ;
#21195=CARTESIAN_POINT ( 'NONE',  ( 0.3613381517857143232, 0.008035714188171892355, 0.1174058825155741975 ) ) ;
#21197=DIRECTION ( 'NONE',  ( 0.000000000000000000, 1.000000000000000000, 0.000000000000000000 ) ) ;
#21205=ADVANCED_FACE ( 'NONE', ( #18087 ), #17854, .T. ) ;
#21243=CARTESIAN_POINT ( 'NONE',  ( 0.2472135954999579721, 0.4017857140906295199, -0.3402603233408159622 ) ) ;
#21263=CARTESIAN_POINT ( 'NONE',  ( -0.2233192592356399442, 0.2330357141881718441, -0.3073725909049500049 ) ) ;
#21266=CARTESIAN_POINT ( 'NONE',  ( -0.1116596296178200276, 0.4187499999024575370, 0.3436530038418508792 ) ) ;
#21278=CARTESIAN_POINT ( 'NONE',  ( 0.2923287055106771337, 0.2723214284738861291, 0.2123892367102621359 ) ) ;
#21284=CARTESIAN_POINT ( 'NONE',  ( -0.3394572874457115752, 3.700000000000000622, 0.09499999999999993172 ) ) ;
#21293=CARTESIAN_POINT ( 'NONE',  ( 0.000000000000000000, 3.700000000000000622, 0.000000000000000000 ) ) ;
#21299=B_SPLINE_CURVE_WITH_KNOTS ( 'NONE', 3,
 ( #22867, #13621, #21040, #15199 ),
 .UNSPECIFIED., .F., .F.,
 ( 4, 4 ),
 ( 1.008999589182314829E-06, 0.001469413801632195879 ),
 .UNSPECIFIED. ) ;
#21314=CARTESIAN_POINT ( 'NONE',  ( 0.3613381517857143232, 0.06160714275960043479, 0.1174058825155742114 ) ) ;
#21321=EDGE_LOOP ( 'NONE', ( #3718, #23056, #16000, #15438, #13271, #1072, #9328, #806, #23190 ) ) ;
#21324=CARTESIAN_POINT ( 'NONE',  ( 0.2472135954999579721, 0.1249999999999999306, -0.3402603233408160732 ) ) ;
#21331=CARTESIAN_POINT ( 'NONE',  ( 0.2285105464130554875, -9.196729208309095321E-18, 0.2808975190895516838 ) ) ;
#21333=VERTEX_POINT ( 'NONE', #15497 ) ;
#21350=DIRECTION ( 'NONE',  ( 0.000000000000000000, 1.000000000000000000, 0.000000000000000000 ) ) ;
#21360=AXIS2_PLACEMENT_3D ( 'NONE', #13991, #21419, #19707 ) ;
#21361=CARTESIAN_POINT ( 'NONE',  ( -0.3613381517857143232, 0.1187499999024576036, -4.425116109941954795E-17 ) ) ;
#21364=CARTESIAN_POINT ( 'NONE',  ( 0.4000000000000000222, 0.1767857140906294589, 0.000000000000000000 ) ) ;
#21370=ORIENTED_EDGE ( 'NONE', *, *, #8118, .T. ) ;
#21371=CIRCLE ( 'NONE', #3459, 0.09499999999999995948 ) ;
#21381=CARTESIAN_POINT ( 'NONE',  ( -0.3613381517857143232, 0.3830357141881717276, -0.1174058825155741004 ) ) ;
#21386=EDGE_LOOP ( 'NONE', ( #20257, #22488, #595, #7851 ) ) ;
#21395=EDGE_CURVE ( 'NONE', #18107, #6978, #2896, .T. ) ;
#21419=DIRECTION ( 'NONE',  ( 0.000000000000000000, 1.000000000000000000, 0.000000000000000000 ) ) ;
#21433=CARTESIAN_POINT ( 'NONE',  ( -0.2923287055106771337, 0.3223214284738861735, 0.2123892367102619971 ) ) ;
#21449=CARTESIAN_POINT ( 'NONE',  ( 0.3233240115537838744, 3.229549314084639149E-17, 0.1617550376952779367 ) ) ;
#21450=( BOUNDED_CURVE ( )  B_SPLINE_CURVE ( 2, ( #9038, #10875, #7095, #14533, #11113, #21955, #16483 ),
 .UNSPECIFIED., .F., .F. ) 
 B_SPLINE_CURVE_WITH_KNOTS ( ( 3, 2, 2, 3 ),
 ( 0.9642857142857143016, 0.9714285714285714191, 0.9857142857142857650, 1.000000000000000000 ),
 .UNSPECIFIED. ) 
 CURVE ( )  GEOMETRIC_REPRESENTATION_ITEM ( )  RATIONAL_B_SPLINE_CURVE ( ( 0.9755282581475768211, 0.9755282581475768211, 1.000000000000000000, 0.9510565162951535312, 1.000000000000000000, 0.9510565162951535312, 1.000000000000000000 ) ) 
 REPRESENTATION_ITEM ( '' )  );
#21451=VERTEX_POINT ( 'NONE', #7515 ) ;
#21462=DIRECTION ( 'NONE',  ( -0.000000000000000000, 1.000000000000000000, -0.000000000000000000 ) ) ;
#21464=CARTESIAN_POINT ( 'NONE',  ( -0.3613381517857143232, -0.02767857152611381821, -0.1174058825155741004 ) ) ;
#21468=CARTESIAN_POINT ( 'NONE',  ( -0.06335377612981472895, 0.1339733671981016006, -0.3999999999999999667 ) ) ;
#21477=CARTESIAN_POINT ( 'NONE',  ( -0.2233192592356399442, 0.03660714275960045422, -0.3073725909049500049 ) ) ;
#21480=CARTESIAN_POINT ( 'NONE',  ( 0.3236067977499790249, 0.1839285712334866041, -0.2351141009169892826 ) ) ;
#21482=EDGE_CURVE ( 'NONE', #16231, #20833, #21299, .T. ) ;
#21496=CARTESIAN_POINT ( 'NONE',  ( 0.2923287055106771337, 0.2723214284738861291, 0.2123892367102621359 ) ) ;
#21522=ORIENTED_EDGE ( 'NONE', *, *, #61, .F. ) ;
#21524=DIRECTION ( 'NONE',  ( 0.000000000000000000, -0.000000000000000000, 1.000000000000000000 ) ) ;
#21539=EDGE_LOOP ( 'NONE', ( #6036, #20744, #4489, #20931, #4611, #11473, #5020, #13010 ) ) ;
#21547=CARTESIAN_POINT ( 'NONE',  ( -6.979263641208234666E-17, 0.1187499999024575897, 0.3799334167787516425 ) ) ;
#21555=CARTESIAN_POINT ( 'NONE',  ( 0.3999999999999999667, 0.1178571428571428131, -0.1299678784931625197 ) ) ;
#21567=CARTESIAN_POINT ( 'NONE',  ( 0.1116596296178199860, 0.008035714188171883682, -0.3436530038418508792 ) ) ;
#21577=CARTESIAN_POINT ( 'NONE',  ( -0.1116596296178200276, -0.009821428668970967266, 0.3436530038418508792 ) ) ;
#21592=CARTESIAN_POINT ( 'NONE',  ( 0.3613381517857143232, 0.01517857133102903065, -0.1174058825155740587 ) ) ;
#21618=CARTESIAN_POINT ( 'NONE',  ( 0.1116596296178199027, 0.2651785713310289561, 0.3436530038418508792 ) ) ;
#21630=CARTESIAN_POINT ( 'NONE',  ( -0.3236067977499790249, 0.2196428569477723025, 0.2351141009169892271 ) ) ;
#21635=ORIENTED_EDGE ( 'NONE', *, *, #13984, .T. ) ;
#21648=ORIENTED_EDGE ( 'NONE', *, *, #7956, .T. ) ;
#21666=B_SPLINE_CURVE_WITH_KNOTS ( 'NONE', 3,
 ( #11981, #4277, #6347, #17329 ),
 .UNSPECIFIED., .F., .F.,
 ( 4, 4 ),
 ( 0.02048720093474762707, 0.02195606945063139845 ),
 .UNSPECIFIED. ) ;
#21673=CARTESIAN_POINT ( 'NONE',  ( 2.326421213736078119E-17, 0.1544642856167433020, -0.3799334167787516425 ) ) ;
#21691=CARTESIAN_POINT ( 'NONE',  ( 4.375590819076689459E-17, 0.01607142837634377430, 0.4000000000000000222 ) ) ;
#21705=CARTESIAN_POINT ( 'NONE',  ( -0.3613381517857143232, 0.1187499999024575897, -4.425116109941954795E-17 ) ) ;
#21719=CARTESIAN_POINT ( 'NONE',  ( -0.3613381517857143232, -0.02410714295468524213, -4.425116109941954795E-17 ) ) ;
#21724=VERTEX_POINT ( 'NONE', #3464 ) ;
#21741=CARTESIAN_POINT ( 'NONE',  ( -0.2923287055106771337, 0.3937499999024575148, 0.2123892367102619971 ) ) ;
#21743=EDGE_CURVE ( 'NONE', #10268, #431, #16521, .T. ) ;
#21767=CARTESIAN_POINT ( 'NONE',  ( -0.06335377612981457629, 0.3803123470876124679, 0.3999999999999999667 ) ) ;
#21786=CARTESIAN_POINT ( 'NONE',  ( 0.2233192592356399164, 0.4294642856167432687, 0.3073725909049500604 ) ) ;
#21788=CARTESIAN_POINT ( 'NONE',  ( 0.3613381517857143232, 0.2830357141881717498, -0.1174058825155740587 ) ) ;
#21797=FACE_OUTER_BOUND ( 'NONE', #4525, .T. ) ;
#21816=DIRECTION ( 'NONE',  ( -0.000000000000000000, -1.000000000000000000, -0.000000000000000000 ) ) ;
#21817=CARTESIAN_POINT ( 'NONE',  ( -0.1116596296178199582, 0.03303571418817188160, -0.3436530038418508792 ) ) ;
#21820=CARTESIAN_POINT ( 'NONE',  ( 0.06335377612981449302, 0.01790193843158826431, 0.4000000000000000222 ) ) ;
#21830=CARTESIAN_POINT ( 'NONE',  ( 0.2923287055106771337, 0.004464285616743319737, 0.2123892367102621359 ) ) ;
#21852=VECTOR ( 'NONE', #3526, 39.37007874015748143 ) ;
#21856=CARTESIAN_POINT ( 'NONE',  ( -0.1236067977499790416, 0.09285714285714280480, 0.3804226065180614236 ) ) ;
#21888=ORIENTED_EDGE ( 'NONE', *, *, #9760, .F. ) ;
#21889=CARTESIAN_POINT ( 'NONE',  ( -0.2977100099089716734, 3.700000000000000622, -0.09499999999999995948 ) ) ;
#21900=ORIENTED_EDGE ( 'NONE', *, *, #8462, .T. ) ;
#21921=CARTESIAN_POINT ( 'NONE',  ( -0.3999999999999999667, 0.2178571428571427493, -0.1299678784931626030 ) ) ;
#21934=CARTESIAN_POINT ( 'NONE',  ( 0.2923287055106771337, 0.01874999990245760501, -0.2123892367102620249 ) ) ;
#21939=CARTESIAN_POINT ( 'NONE',  ( -0.1236067977499790416, 0.1642857142857142294, 0.3804226065180614236 ) ) ;
#21949=CARTESIAN_POINT ( 'NONE',  ( 0.1116596296178199860, 0.3116071427596003862, -0.3436530038418508792 ) ) ;
#21954=ORIENTED_EDGE ( 'NONE', *, *, #19928, .F. ) ;
#21955=CARTESIAN_POINT ( 'NONE',  ( 0.3999999999999999667, 0.3964285714285711859, 0.1299678784931626307 ) ) ;
#21958=CIRCLE ( 'NONE', #2533, 0.3125000000000000000 ) ;
#21960=CARTESIAN_POINT ( 'NONE',  ( 0.3236067977499790249, 0.2553571426620580009, -0.2351141009169892826 ) ) ;
#21974=CARTESIAN_POINT ( 'NONE',  ( -7.726019084026502927E-17, -0.04642857142857145097, 0.4205848896953069405 ) ) ;
#21980=CARTESIAN_POINT ( 'NONE',  ( 0.2977100099089716734, 3.575000000000000622, -0.09499999999999993172 ) ) ;
#22017=AXIS2_PLACEMENT_3D ( 'NONE', #17773, #13999, #4956 ) ;
#22019=PLANE ( 'NONE',  #2730 ) ;
#22027=VECTOR ( 'NONE', #6645, 39.37007874015748143 ) ;
#22028=CARTESIAN_POINT ( 'NONE',  ( 0.3999999999999999667, 0.04642857142857139546, -0.1299678784931625197 ) ) ;
#22044=LINE ( 'NONE', #1801, #20981 ) ;
#22059=CARTESIAN_POINT ( 'NONE',  ( 0.2923287055106771337, 0.3616071427596004306, 0.2123892367102621359 ) ) ;
#22060=AXIS2_PLACEMENT_3D ( 'NONE', #17331, #15030, #22455 ) ;
#22071=CARTESIAN_POINT ( 'NONE',  ( 2.326421213736078119E-17, 0.3151785713310290005, -0.3799334167787516425 ) ) ;
#22090=EDGE_LOOP ( 'NONE', ( #7457, #4327, #10417, #7403 ) ) ;
#22091=EDGE_LOOP ( 'NONE', ( #13333, #3014, #18941, #23934 ) ) ;
#22095=CARTESIAN_POINT ( 'NONE',  ( 0.3999999999999999667, -0.09642857142857144681, -0.1299678784931625475 ) ) ;
#22102=CARTESIAN_POINT ( 'NONE',  ( 0.3236067977499790249, 0.04107142837634378957, -0.2351141009169892826 ) ) ;
#22125=CARTESIAN_POINT ( 'NONE',  ( -6.979263641208234666E-17, 0.06517857133102902822, 0.3799334167787516980 ) ) ;
#22148=CIRCLE ( 'NONE', #8518, 0.3525000000000007017 ) ;
#22164=DIRECTION ( 'NONE',  ( -0.000000000000000000, -1.000000000000000000, -0.000000000000000000 ) ) ;
#22178=CARTESIAN_POINT ( 'NONE',  ( -0.1116596296178200276, 0.3473214284738860846, 0.3436530038418508792 ) ) ;
#22191=CARTESIAN_POINT ( 'NONE',  ( 0.2233192592356399997, 0.2366071427596004029, -0.3073725909049500049 ) ) ;
#22194=CARTESIAN_POINT ( 'NONE',  ( 0.4749999999999999778, 3.575000000000000622, 2.908536147974959276E-17 ) ) ;
#22202=CARTESIAN_POINT ( 'NONE',  ( -7.000945310522701902E-17, 0.2303571426620580065, 0.3999999999999999667 ) ) ;
#22213=CARTESIAN_POINT ( 'NONE',  ( 0.3613381517857143232, 0.4223214284738860957, 0.000000000000000000 ) ) ;
#22221=CARTESIAN_POINT ( 'NONE',  ( -0.1236067977499790416, 0.01249999980491522077, 0.3804226065180614236 ) ) ;
#22243=CARTESIAN_POINT ( 'NONE',  ( 0.2923287055106771337, -0.07053571438325667575, -0.2123892367102620249 ) ) ;
#22247=CARTESIAN_POINT ( 'NONE',  ( -0.1116596296178199582, 0.1044642856167433131, -0.3436530038418508792 ) ) ;
#22257=DIRECTION ( 'NONE',  ( 0.000000000000000000, 0.000000000000000000, -1.000000000000000000 ) ) ;
#22262=CARTESIAN_POINT ( 'NONE',  ( -0.3613381517857143232, 0.1687499999024575370, -0.1174058825155741143 ) ) ;
#22290=VERTEX_POINT ( 'NONE', #20112 ) ;
#22297=CARTESIAN_POINT ( 'NONE',  ( -0.3613381517857143232, 0.3330357141881718497, -4.425116109941954795E-17 ) ) ;
#22309=CARTESIAN_POINT ( 'NONE',  ( 2.326421213736078119E-17, 0.1723214284738861790, -0.3799334167787516425 ) ) ;
#22313=CARTESIAN_POINT ( 'NONE',  ( 0.3236067977499790249, 0.3982142855192009057, -0.2351141009169892826 ) ) ;
#22331=CARTESIAN_POINT ( 'NONE',  ( -0.2472135954999579999, 0.3035714285714284921, 0.3402603233408159622 ) ) ;
#22338=CARTESIAN_POINT ( 'NONE',  ( 0.1236067977499789861, -0.02321428590937048980, -0.3804226065180614236 ) ) ;
#22358=CARTESIAN_POINT ( 'NONE',  ( 0.1891708636127259202, 2.539511724522405989E-17, 0.3078630284654709781 ) ) ;
#22361=CARTESIAN_POINT ( 'NONE',  ( 0.1116596296178199860, -0.06339285724039953052, -0.3436530038418508792 ) ) ;
#22365=CARTESIAN_POINT ( 'NONE',  ( 0.1116596296178199860, 0.1687499999024575925, -0.3436530038418508792 ) ) ;
#22377=LINE ( 'NONE', #187, #12476 ) ;
#22378=CARTESIAN_POINT ( 'NONE',  ( 0.3613381517857143232, 0.2080357141881718774, 0.000000000000000000 ) ) ;
#22396=CARTESIAN_POINT ( 'NONE',  ( -0.2472135954999579999, 0.4374999998049151073, 0.3402603233408160732 ) ) ;
#22399=CARTESIAN_POINT ( 'NONE',  ( -0.3236067977499789694, 0.06249999980491519752, -0.2351141009169893104 ) ) ;
#22400=DIRECTION ( 'NONE',  ( -0.000000000000000000, 1.000000000000000000, -0.000000000000000000 ) ) ;
#22409=DIRECTION ( 'NONE',  ( 0.8660254037844394848, 0.4999999999999983902, -0.000000000000000000 ) ) ;
#22421=CARTESIAN_POINT ( 'NONE',  ( 2.326421213736078119E-17, 0.2437499999024574926, -0.3799334167787516425 ) ) ;
#22424=CARTESIAN_POINT ( 'NONE',  ( 0.06335377612981453466, 0.04995520403538498966, -0.3999999999999999667 ) ) ;
#22428=DIRECTION ( 'NONE',  ( 0.000000000000000000, 1.000000000000000000, 0.000000000000000000 ) ) ;
#22432=CARTESIAN_POINT ( 'NONE',  ( 0.2233192592356399164, 0.2151785713310289949, 0.3073725909049500604 ) ) ;
#22439=CARTESIAN_POINT ( 'NONE',  ( 0.1236067977499789028, 0.3053571426620579898, 0.3804226065180614791 ) ) ;
#22455=DIRECTION ( 'NONE',  ( 1.000000000000000000, 0.000000000000000000, 0.000000000000000000 ) ) ;
#22457=CARTESIAN_POINT ( 'NONE',  ( 0.3236067977499789694, 0.3214285714285713413, 0.2351141009169893659 ) ) ;
#22464=CARTESIAN_POINT ( 'NONE',  ( -0.3999999999999999667, -0.005357143052227637120, -0.1299678784931626030 ) ) ;
#22475=VERTEX_POINT ( 'NONE', #19237 ) ;
#22484=CARTESIAN_POINT ( 'NONE',  ( -0.4749999999999999778, 3.575000000000000622, -0.09499999999999995948 ) ) ;
#22486=CARTESIAN_POINT ( 'NONE',  ( -0.2233192592356399442, -0.05267857152611380572, -0.3073725909049500049 ) ) ;
#22488=ORIENTED_EDGE ( 'NONE', *, *, #19439, .T. ) ;
#22489=CARTESIAN_POINT ( 'NONE',  ( -0.3613381517857143232, 0.1901785713310290282, -4.425116109941954795E-17 ) ) ;
#22502=CARTESIAN_POINT ( 'NONE',  ( 0.1116596296178199027, 0.1937499999024575870, 0.3436530038418508792 ) ) ;
#22521=CARTESIAN_POINT ( 'NONE',  ( -0.06335377612981447915, 0.08566948974967070196, 0.4000000000000000777 ) ) ;
#22522=ADVANCED_FACE ( 'NONE', ( #16066, #17896 ), #6671, .F. ) ;
#22531=VERTEX_POINT ( 'NONE', #3134 ) ;
#22545=CARTESIAN_POINT ( 'NONE',  ( 0.2233192592356399997, 0.2366071427596003751, -0.3073725909049500049 ) ) ;
#22557=CARTESIAN_POINT ( 'NONE',  ( 9.101228903679513089E-16, 0.3732142855192008835, 0.4000000000000000222 ) ) ;
#22566=DIRECTION ( 'NONE',  ( -0.000000000000000000, -1.000000000000000000, -0.000000000000000000 ) ) ;
#22578=CARTESIAN_POINT ( 'NONE',  ( -0.06335377612981449302, 0.3393305098601595571, -0.4000000000000000222 ) ) ;
#22579=CARTESIAN_POINT ( 'NONE',  ( -0.2472135954999579999, 0.1607142857142856429, 0.3402603233408159622 ) ) ;
#22589=CARTESIAN_POINT ( 'NONE',  ( 0.4000000000000000222, 0.1767857140906294866, 0.000000000000000000 ) ) ;
#22593=CYLINDRICAL_SURFACE ( 'NONE', #6733, 0.4000000000000000222 ) ;
#22598=CARTESIAN_POINT ( 'NONE',  ( -0.1236067977499789583, 0.2696428569477722914, -0.3804226065180614791 ) ) ;
#22614=CARTESIAN_POINT ( 'NONE',  ( -0.2923287055106771337, 0.03660714275960045422, 0.2123892367102619971 ) ) ;
#22616=ORIENTED_EDGE ( 'NONE', *, *, #4975, .F. ) ;
#22617=CARTESIAN_POINT ( 'NONE',  ( -0.2233192592356400275, 0.3437499999024575259, 0.3073725909049499494 ) ) ;
#22622=CARTESIAN_POINT ( 'NONE',  ( 0.000000000000000000, 3.700000000000000622, -0.4000000000000000222 ) ) ;
#22631=CARTESIAN_POINT ( 'NONE',  ( -0.2233192592356400275, 0.1830357141881718552, 0.3073725909049499494 ) ) ;
#22663=CARTESIAN_POINT ( 'NONE',  ( 0.1116596296178199860, 0.008035714188171883682, -0.3436530038418508792 ) ) ;
#22675=CARTESIAN_POINT ( 'NONE',  ( 0.3999999999999999667, 0.3874999998049150629, 0.1299678784931626307 ) ) ;
#22688=EDGE_CURVE ( 'NONE', #22475, #5943, #8730, .T. ) ;
#22695=CARTESIAN_POINT ( 'NONE',  ( -0.2472135954999579444, 0.1392857142857142350, -0.3402603233408159622 ) ) ;
#22703=CARTESIAN_POINT ( 'NONE',  ( -0.2472135954999579444, 0.3446428569477723025, -0.3402603233408159622 ) ) ;
#22708=PLANE ( 'NONE',  #15951 ) ;
#22719=VERTEX_POINT ( 'NONE', #11551 ) ;
#22725=CARTESIAN_POINT ( 'NONE',  ( 0.1116596296178199860, 0.07946428561674331870, -0.3436530038418508792 ) ) ;
#22730=CARTESIAN_POINT ( 'NONE',  ( 0.3613381517857143232, 0.4366071427596003862, 0.1174058825155741975 ) ) ;
#22744=CARTESIAN_POINT ( 'NONE',  ( 0.1116596296178199027, 0.1223214284738861762, 0.3436530038418508792 ) ) ;
#22780=CARTESIAN_POINT ( 'NONE',  ( -0.2233192592356399997, 0.4151785713310289783, 0.3073725909049499494 ) ) ;
#22783=DIRECTION ( 'NONE',  ( 0.000000000000000000, 1.000000000000000000, 0.000000000000000000 ) ) ;
#22787=CARTESIAN_POINT ( 'NONE',  ( 0.2472135954999579721, 0.1160714283763437660, -0.3402603233408160732 ) ) ;
#22794=CARTESIAN_POINT ( 'NONE',  ( 0.000000000000000000, 3.700000000000000622, 0.000000000000000000 ) ) ;
#22795=CARTESIAN_POINT ( 'NONE',  ( 8.817456953860933428E-17, 3.700000000000000622, 0.7199999999999994182 ) ) ;
#22800=CARTESIAN_POINT ( 'NONE',  ( 0.2233192592356399164, 0.4116071427596004195, 0.3073725909049500604 ) ) ;
#22816=CARTESIAN_POINT ( 'NONE',  ( 0.3236067977499789694, 0.1071428571428571092, 0.2351141009169893659 ) ) ;
#22823=CARTESIAN_POINT ( 'NONE',  ( -0.4000000000000000222, 0.2839285712334865819, -4.898587196589413075E-17 ) ) ;
#22846=CARTESIAN_POINT ( 'NONE',  ( 0.2233192592356399997, 0.07589285704531473220, -0.3073725909049500049 ) ) ;
#22849=CARTESIAN_POINT ( 'NONE',  ( -0.3613381517857143232, 0.4044642856167432465, -4.425116109941954795E-17 ) ) ;
#22851=DIMENSIONAL_EXPONENTS ( 1.000000000000000000, 0.000000000000000000, 0.000000000000000000, 0.000000000000000000, 0.000000000000000000, 0.000000000000000000, 0.000000000000000000 ) ;
#22861=CARTESIAN_POINT ( 'NONE',  ( 2.326421213736078119E-17, 0.2973214284738861513, -0.3799334167787516980 ) ) ;
#22863=ORIENTED_EDGE ( 'NONE', *, *, #20735, .F. ) ;
#22867=CARTESIAN_POINT ( 'NONE',  ( 0.3394572874457115752, 3.700000000000000622, -0.09499999999999993172 ) ) ;
#22883=EDGE_CURVE ( 'NONE', #17619, #5247, #11918, .T. ) ;
#22889=EDGE_LOOP ( 'NONE', ( #12153, #8039, #17121, #306 ) ) ;
#22895=AXIS2_PLACEMENT_3D ( 'NONE', #9956, #19091, #13622 ) ;
#22898=CARTESIAN_POINT ( 'NONE',  ( 0.3613381517857143232, 0.4366071427596004417, 0.1174058825155742114 ) ) ;
#22901=LINE ( 'NONE', #13414, #14690 ) ;
#22914=CARTESIAN_POINT ( 'NONE',  ( 0.2786222087057687591, 1.697684548454547126E-17, 0.2312824624941703378 ) ) ;
#22916=AXIS2_PLACEMENT_3D ( 'NONE', #23634, #21816, #5106 ) ;
#22920=CARTESIAN_POINT ( 'NONE',  ( 0.1116596296178199027, 0.4080357141881718608, 0.3436530038418508792 ) ) ;
#22921=LINE ( 'NONE', #20973, #16156 ) ;
#22939=CARTESIAN_POINT ( 'NONE',  ( -0.1236067977499789583, 0.2696428569477723469, -0.3804226065180614791 ) ) ;
#22942=ORIENTED_EDGE ( 'NONE', *, *, #15431, .T. ) ;
#22946=ORIENTED_EDGE ( 'NONE', *, *, #8802, .T. ) ;
#22948=CARTESIAN_POINT ( 'NONE',  ( 0.3236067977499789694, 0.3214285714285713413, 0.2351141009169893659 ) ) ;
#22950=ORIENTED_EDGE ( 'NONE', *, *, #935, .F. ) ;
#22952=ORIENTED_EDGE ( 'NONE', *, *, #21395, .T. ) ;
#22957=CARTESIAN_POINT ( 'NONE',  ( 0.3613381517857143232, 0.2794642856167433020, 0.000000000000000000 ) ) ;
#22959=VECTOR ( 'NONE', #20895, 39.37007874015748143 ) ;
#22961=CARTESIAN_POINT ( 'NONE',  ( -6.979263641208234666E-17, 0.3508928570453145879, 0.3799334167787516980 ) ) ;
#22972=CARTESIAN_POINT ( 'NONE',  ( -0.3613381517857143232, 0.2401785713310289616, -0.1174058825155741143 ) ) ;
#22990=DIRECTION ( 'NONE',  ( 0.000000000000000000, 0.000000000000000000, -1.000000000000000000 ) ) ;
#23000=CARTESIAN_POINT ( 'NONE',  ( -0.3255746763033851021, 3.686631053841027850, 0.09499999999999995948 ) ) ;
#23012=CARTESIAN_POINT ( 'NONE',  ( -0.2923287055106771337, 0.02232142847388617762, -0.2123892367102620804 ) ) ;
#23015=CARTESIAN_POINT ( 'NONE',  ( 0.2502152602304669737, 0.002284799041592490421, 0.2703534214026953597 ) ) ;
#23021=CARTESIAN_POINT ( 'NONE',  ( 1.750236327630675537E-16, 0.08749999980491518503, 0.3999999999999999667 ) ) ;
#23032=CARTESIAN_POINT ( 'NONE',  ( -0.1116596296178200276, 0.3294642856167432354, 0.3436530038418508792 ) ) ;
#23044=DIRECTION ( 'NONE',  ( 0.000000000000000000, 0.000000000000000000, -1.000000000000000000 ) ) ;
#23052=CARTESIAN_POINT ( 'NONE',  ( -0.4000000000000000222, 0.3553571426620580342, -4.898587196589413075E-17 ) ) ;
#23056=ORIENTED_EDGE ( 'NONE', *, *, #6029, .T. ) ;
#23073=CARTESIAN_POINT ( 'NONE',  ( 0.1116596296178199027, 0.3366071427596004084, 0.3436530038418508792 ) ) ;
#23076=CARTESIAN_POINT ( 'NONE',  ( -6.979263641208234666E-17, 0.2794642856167432465, 0.3799334167787516980 ) ) ;
#23088=CARTESIAN_POINT ( 'NONE',  ( 0.2233192592356399164, 0.2687499999024575703, 0.3073725909049500604 ) ) ;
#23103=FACE_OUTER_BOUND ( 'NONE', #22091, .T. ) ;
#23115=CARTESIAN_POINT ( 'NONE',  ( 0.000000000000000000, 3.669999999999999929, 0.000000000000000000 ) ) ;
#23116=VERTEX_POINT ( 'NONE', #7261 ) ;
#23119=CARTESIAN_POINT ( 'NONE',  ( -9.626299801968715084E-16, 0.3464285714285713635, -0.4000000000000000222 ) ) ;
#23122=CARTESIAN_POINT ( 'NONE',  ( -0.1116596296178200276, 0.04374999990245760639, 0.3436530038418508792 ) ) ;
#23126=CARTESIAN_POINT ( 'NONE',  ( 0.000000000000000000, 0.000000000000000000, 0.000000000000000000 ) ) ;
#23144=CARTESIAN_POINT ( 'NONE',  ( 0.2233192592356399164, 0.3401785713310290227, 0.3073725909049500604 ) ) ;
#23159=CARTESIAN_POINT ( 'NONE',  ( -0.3236067977499790249, 0.3714285714285713302, 0.2351141009169892271 ) ) ;
#23162=ADVANCED_FACE ( 'NONE', ( #9206 ), #11846, .T. ) ;
#23167=CARTESIAN_POINT ( 'NONE',  ( 0.2472135954999579166, 0.3089285712334866041, 0.3402603233408160732 ) ) ;
#23172=CARTESIAN_POINT ( 'NONE',  ( 0.3236067977499789694, 0.1696428569477723136, 0.2351141009169893659 ) ) ;
#23181=DIRECTION ( 'NONE',  ( 0.000000000000000000, 0.000000000000000000, 1.000000000000000000 ) ) ;
#23190=ORIENTED_EDGE ( 'NONE', *, *, #1615, .F. ) ;
#23194=CARTESIAN_POINT ( 'NONE',  ( -0.1116596296178199582, 0.3723214284738861068, -0.3436530038418508792 ) ) ;
#23195=CARTESIAN_POINT ( 'NONE',  ( 0.000000000000000000, 2.735000000000000320, 0.7500000000000001110 ) ) ;
#23214=EDGE_CURVE ( 'NONE', #14906, #431, #610, .T. ) ;
#23230=CARTESIAN_POINT ( 'NONE',  ( 9.101228903679513089E-16, 0.3107142857142856096, 0.4000000000000000222 ) ) ;
#23241=CARTESIAN_POINT ( 'NONE',  ( -0.2233192592356399442, 0.2330357141881718441, -0.3073725909049500049 ) ) ;
#23244=DIRECTION ( 'NONE',  ( -0.000000000000000000, -1.000000000000000000, -0.000000000000000000 ) ) ;
#23247=ORIENTED_EDGE ( 'NONE', *, *, #7063, .T. ) ;
#23259=LINE ( 'NONE', #2561, #516 ) ;
#23273=CARTESIAN_POINT ( 'NONE',  ( 0.1116596296178199027, 0.1401785713310290116, 0.3436530038418508792 ) ) ;
#23285=CARTESIAN_POINT ( 'NONE',  ( 0.1236067977499789028, 0.4482142855192008946, 0.3804226065180614791 ) ) ;
#23294=DIRECTION ( 'NONE',  ( 1.000000000000000000, 0.000000000000000000, 0.000000000000000000 ) ) ;
#23311=CARTESIAN_POINT ( 'NONE',  ( 0.3613381517857143232, 0.2116071427596004084, -0.1174058825155740587 ) ) ;
#23313=DIRECTION ( 'NONE',  ( 0.000000000000000000, 1.000000000000000000, 0.000000000000000000 ) ) ;
#23335=EDGE_LOOP ( 'NONE', ( #6035, #15006 ) ) ;
#23337=DIRECTION ( 'NONE',  ( 0.000000000000000000, 1.000000000000000000, 0.000000000000000000 ) ) ;
#23339=ORIENTED_EDGE ( 'NONE', *, *, #17335, .F. ) ;
#23350=ADVANCED_BREP_SHAPE_REPRESENTATION ( '', ( #1082, #9127 ), #7955 ) ;
#23356=UNCERTAINTY_MEASURE_WITH_UNIT (LENGTH_MEASURE( 1.000000000000000082E-05 ), #17469, 'distance_accuracy_value', 'NONE');
#23363=CARTESIAN_POINT ( 'NONE',  ( -0.3613381517857143232, 0.1687499999024575370, -0.1174058825155741004 ) ) ;
#23367=DIRECTION ( 'NONE',  ( 0.000000000000000000, 0.000000000000000000, -1.000000000000000000 ) ) ;
#23369=CARTESIAN_POINT ( 'NONE',  ( 0.000000000000000000, 0.02999999999999995379, 0.000000000000000000 ) ) ;
#23396=CARTESIAN_POINT ( 'NONE',  ( 0.1116596296178199860, 0.02589285704531473636, -0.3436530038418508792 ) ) ;
#23401=CARTESIAN_POINT ( 'NONE',  ( 0.000000000000000000, 3.575000000000000622, 0.000000000000000000 ) ) ;
#23409=CARTESIAN_POINT ( 'NONE',  ( -0.2472135954999579999, 0.4374999998049151628, 0.3402603233408159622 ) ) ;
#23413=CARTESIAN_POINT ( 'NONE',  ( 0.2472135954999579721, 0.1874999998049151628, -0.3402603233408160732 ) ) ;
#23432=CARTESIAN_POINT ( 'NONE',  ( 0.2923287055106771337, 0.2151785713310289949, -0.2123892367102620249 ) ) ;
#23438=DIRECTION ( 'NONE',  ( 0.000000000000000000, 1.000000000000000000, 0.000000000000000000 ) ) ;
#23444=VERTEX_POINT ( 'NONE', #8606 ) ;
#23464=CIRCLE ( 'NONE', #16089, 0.09499999999999995948 ) ;
#23478=CARTESIAN_POINT ( 'NONE',  ( 0.1116596296178199027, 0.3544642856167432576, 0.3436530038418508792 ) ) ;
#23481=CARTESIAN_POINT ( 'NONE',  ( -0.2923287055106771337, 0.2508928570453147211, 0.2123892367102619971 ) ) ;
#23486=DIRECTION ( 'NONE',  ( -0.000000000000000000, -1.000000000000000000, -0.000000000000000000 ) ) ;
#23489=CARTESIAN_POINT ( 'NONE',  ( 0.3236067977499789694, 0.1071428571428571092, 0.2351141009169893659 ) ) ;
#23512=CARTESIAN_POINT ( 'NONE',  ( -0.2923287055106771337, -0.01696428581182811424, 0.2123892367102619971 ) ) ;
#23519=ORIENTED_EDGE ( 'NONE', *, *, #7985, .T. ) ;
#23524=CARTESIAN_POINT ( 'NONE',  ( -0.2923287055106771337, 0.05446428561674331731, 0.2123892367102619971 ) ) ;
#23528=DIRECTION ( 'NONE',  ( -0.000000000000000000, -1.000000000000000000, -0.000000000000000000 ) ) ;
#23550=CARTESIAN_POINT ( 'NONE',  ( -0.4000000000000000222, 0.08214285714285710083, 0.1299678784931624920 ) ) ;
#23551=DIRECTION ( 'NONE',  ( 0.000000000000000000, 0.000000000000000000, -1.000000000000000000 ) ) ;
#23566=ORIENTED_EDGE ( 'NONE', *, *, #9178, .F. ) ;
#23587=CARTESIAN_POINT ( 'NONE',  ( -9.626299801968715084E-16, 0.4089285712334866374, -0.4000000000000000222 ) ) ;
#23593=CARTESIAN_POINT ( 'NONE',  ( -0.2923287055106771337, 0.2544642856167432798, -0.2123892367102620804 ) ) ;
#23597=CARTESIAN_POINT ( 'NONE',  ( 0.000000000000000000, 2.735000000000000320, -0.4000000000000000222 ) ) ;
#23600=CARTESIAN_POINT ( 'NONE',  ( -0.2233192592356399442, 0.3223214284738860624, -0.3073725909049500049 ) ) ;
#23603=EDGE_CURVE ( 'NONE', #14906, #4381, #9213, .T. ) ;
#23605=CARTESIAN_POINT ( 'NONE',  ( 0.3613381517857143232, 0.1366071427596004251, 0.000000000000000000 ) ) ;
#23613=DIRECTION ( 'NONE',  ( 0.000000000000000000, 0.000000000000000000, 1.000000000000000000 ) ) ;
#23617=VECTOR ( 'NONE', #14640, 39.37007874015748143 ) ;
#23634=CARTESIAN_POINT ( 'NONE',  ( 0.000000000000000000, 3.700000000000000622, 0.000000000000000000 ) ) ;
#23635=CARTESIAN_POINT ( 'NONE',  ( -6.979263641208234666E-17, -0.006250000097542401586, 0.3799334167787516425 ) ) ;
#23646=CARTESIAN_POINT ( 'NONE',  ( -0.1116596296178200276, 0.06160714275960046254, 0.3436530038418508792 ) ) ;
#23647=EDGE_CURVE ( 'NONE', #45, #4381, #15408, .T. ) ;
#23651=ORIENTED_EDGE ( 'NONE', *, *, #19200, .T. ) ;
#23664=AXIS2_PLACEMENT_3D ( 'NONE', #9712, #17149, #439 ) ;
#23669=CARTESIAN_POINT ( 'NONE',  ( -0.2472135954999579999, 0.08928571428571425994, 0.3402603233408159622 ) ) ;
#23673=FACE_OUTER_BOUND ( 'NONE', #66, .T. ) ;
#23691=ORIENTED_EDGE ( 'NONE', *, *, #19956, .F. ) ;
#23716=CARTESIAN_POINT ( 'NONE',  ( -0.2233192592356399997, 0.3437499999024575814, 0.3073725909049499494 ) ) ;
#23721=CARTESIAN_POINT ( 'NONE',  ( -0.2233192592356399997, 0.1116071427596004306, 0.3073725909049499494 ) ) ;
#23728=CARTESIAN_POINT ( 'NONE',  ( -0.4749999999999999778, 3.575000000000000622, -0.09499999999999995948 ) ) ;
#23735=CARTESIAN_POINT ( 'NONE',  ( -0.3236067977499789694, 0.2142857142857142461, -0.2351141009169893104 ) ) ;
#23753=CARTESIAN_POINT ( 'NONE',  ( -0.2923287055106771337, 0.1116071427596004306, -0.2123892367102620804 ) ) ;
#23757=CARTESIAN_POINT ( 'NONE',  ( -7.000945310522701902E-17, 0.1678571428571427882, 0.3999999999999999667 ) ) ;
#23766=CARTESIAN_POINT ( 'NONE',  ( -0.3613381517857143232, 0.1151785713310290032, -0.1174058825155741004 ) ) ;
#23790=CARTESIAN_POINT ( 'NONE',  ( -0.3236067977499789694, -1.707404996040164512E-17, -0.2351141009169893104 ) ) ;
#23796=FACE_BOUND ( 'NONE', #21321, .T. ) ;
#23835=ORIENTED_EDGE ( 'NONE', *, *, #1891, .T. ) ;
#23839=CARTESIAN_POINT ( 'NONE',  ( -0.3613381517857143232, 0.4044642856167432465, -4.425116109941954795E-17 ) ) ;
#23842=CARTESIAN_POINT ( 'NONE',  ( 0.1236067977499789861, 0.05714285714285712720, -0.3804226065180614236 ) ) ;
#23843=CARTESIAN_POINT ( 'NONE',  ( 0.2233192592356399997, 0.3616071427596004861, -0.3073725909049500049 ) ) ;
#23862=ORIENTED_EDGE ( 'NONE', *, *, #15431, .F. ) ;
#23872=CARTESIAN_POINT ( 'NONE',  ( 2.326421213736078119E-17, 0.3151785713310290005, -0.3799334167787516425 ) ) ;
#23878=AXIS2_PLACEMENT_3D ( 'NONE', #4402, #6230, #17454 ) ;
#23886=CARTESIAN_POINT ( 'NONE',  ( 0.3613381517857143232, 0.2294642856167433131, -0.1174058825155740587 ) ) ;
#23910=CARTESIAN_POINT ( 'NONE',  ( 0.3999999999999999667, 0.03928571428571425023, 0.1299678784931626307 ) ) ;
#23918=CARTESIAN_POINT ( 'NONE',  ( 0.3236067977499789694, 0.09821428551920091676, 0.2351141009169893659 ) ) ;
#23924=DIRECTION ( 'NONE',  ( -0.000000000000000000, -1.000000000000000000, -0.000000000000000000 ) ) ;
#23934=ORIENTED_EDGE ( 'NONE', *, *, #7098, .T. ) ;
#23950=CARTESIAN_POINT ( 'NONE',  ( -0.2923287055106771337, 0.1973214284738861179, 0.2123892367102619971 ) ) ;
#23973=CARTESIAN_POINT ( 'NONE',  ( 0.3613381517857143232, 0.4223214284738860957, 0.000000000000000000 ) ) ;
#23996=EDGE_CURVE ( 'NONE', #3037, #13969, #6199, .T. ) ;
#24001=CARTESIAN_POINT ( 'NONE',  ( -6.979263641208234666E-17, 0.2080357141881717942, 0.3799334167787516425 ) ) ;
#24015=CARTESIAN_POINT ( 'NONE',  ( 0.3613381517857143232, 0.1508928570453147155, 0.1174058825155742114 ) ) ;
#24023=AXIS2_PLACEMENT_3D ( 'NONE', #15941, #23244, #23367 ) ;
#24024=CARTESIAN_POINT ( 'NONE',  ( -0.4749999999999999778, 3.700000000000000622, -0.09499999999999995948 ) ) ;
#24036=CARTESIAN_POINT ( 'NONE',  ( 0.3236067977499790249, -0.09285714285714286031, -0.2351141009169892826 ) ) ;
#24044=CARTESIAN_POINT ( 'NONE',  ( 0.4000000000000000222, 0.1053571426620580620, 0.000000000000000000 ) ) ;
#24054=EDGE_LOOP ( 'NONE', ( #9097, #12708, #17496, #13538 ) ) ;
#24066=CARTESIAN_POINT ( 'NONE',  ( 0.3613381517857143232, -0.07767857152611380711, 0.000000000000000000 ) ) ;
#24071=CARTESIAN_POINT ( 'NONE',  ( -0.3613381517857143788, 0.05089285704531475163, 0.1174058825155740310 ) ) ;
#24081=AXIS2_PLACEMENT_3D ( 'NONE', #1258, #6504, #23551 ) ;
#24088=ORIENTED_EDGE ( 'NONE', *, *, #1309, .F. ) ;
#24095=CARTESIAN_POINT ( 'NONE',  ( 2.326421213736078119E-17, 0.3687499999024574371, -0.3799334167787516425 ) ) ;
#24102=CARTESIAN_POINT ( 'NONE',  ( -0.06335377612981449302, 0.05361622414587396968, -0.4000000000000000222 ) ) ;
#24118=CARTESIAN_POINT ( 'NONE',  ( -0.2233192592356399442, 0.3223214284738860624, -0.3073725909049500049 ) ) ;
#24145=COLOUR_RGB('Light Blue', 0.31764706, 0.68627451, 0.89019608);
#24146=FILL_AREA_STYLE_COLOUR('',#24145);
#24147=FILL_AREA_STYLE('',(#24146));
#24148=SURFACE_STYLE_FILL_AREA(#24147);
#24149=SURFACE_SIDE_STYLE('',(#24148));
#24150=SURFACE_STYLE_USAGE(.BOTH.,#24149);
#24151=PRESENTATION_STYLE_ASSIGNMENT((#24150));
#24196=STYLED_ITEM('',(#24151),#1082);
#24197=MECHANICAL_DESIGN_GEOMETRIC_PRESENTATION_REPRESENTATION('',(#24196),#7955);
ENDSEC;
END-ISO-10303-21;
